ISO-10303-21;
HEADER;
/* Generated by software containing ST-Developer
 * from STEP Tools, Inc. (www.steptools.com) 
 */

FILE_DESCRIPTION(
/* description */ (''),
/* implementation_level */ '2;1');

FILE_NAME(
/* name */ '11_Control_Ball_Stud_M2.5_D5.5.step',
/* time_stamp */ '2026-10-25T01:35:35-07:00',
/* author */ (''),
/* organization */ (''),
/* preprocessor_version */ 'ST-DEVELOPER v20.2',
/* originating_system */ 'Autodesk Translation Framework v15.15.0.0',
/* authorisation */ '');

FILE_SCHEMA (('AUTOMOTIVE_DESIGN { 1 0 10303 214 3 1 1 }'));
ENDSEC;

DATA;
#10=MECHANICAL_DESIGN_GEOMETRIC_PRESENTATION_REPRESENTATION('',(#266),#11430);
#79=SPHERICAL_SURFACE('',#4882,2.75);
#82=B_SPLINE_SURFACE_WITH_KNOTS('',3,3,((#8355,#8356,#8357,#8358,#8359,
#8360,#8361,#8362,#8363,#8364,#8365,#8366,#8367,#8368,#8369,#8370,#8371,
#8372,#8373,#8374,#8375,#8376,#8377,#8378,#8379,#8380,#8381,#8382,#8383,
#8384,#8385,#8386,#8387,#8388,#8389,#8390,#8391),(#8392,#8393,#8394,#8395,
#8396,#8397,#8398,#8399,#8400,#8401,#8402,#8403,#8404,#8405,#8406,#8407,
#8408,#8409,#8410,#8411,#8412,#8413,#8414,#8415,#8416,#8417,#8418,#8419,
#8420,#8421,#8422,#8423,#8424,#8425,#8426,#8427,#8428),(#8429,#8430,#8431,
#8432,#8433,#8434,#8435,#8436,#8437,#8438,#8439,#8440,#8441,#8442,#8443,
#8444,#8445,#8446,#8447,#8448,#8449,#8450,#8451,#8452,#8453,#8454,#8455,
#8456,#8457,#8458,#8459,#8460,#8461,#8462,#8463,#8464,#8465),(#8466,#8467,
#8468,#8469,#8470,#8471,#8472,#8473,#8474,#8475,#8476,#8477,#8478,#8479,
#8480,#8481,#8482,#8483,#8484,#8485,#8486,#8487,#8488,#8489,#8490,#8491,
#8492,#8493,#8494,#8495,#8496,#8497,#8498,#8499,#8500,#8501,#8502)),
 .UNSPECIFIED.,.F.,.F.,.F.,(4,4),(4,1,1,1,1,1,1,1,1,1,1,1,1,1,1,1,1,1,1,
1,1,1,1,1,1,1,1,1,1,1,1,1,1,1,4),(0.,0.0296469363228873),(8.30626835282493,
9.28498110675177,10.2636938606786,11.2424066146055,12.2211193685323,13.1998321224591,
14.178544876386,15.1572576303128,16.1359703842396,17.1146831381665,18.0933958920933,
19.0721086460202,20.050821399947,21.0295341538738,22.0082469078007,22.9869596617275,
23.9656724156544,24.9443851695812,25.923097923508,26.9018106774349,27.8805234313617,
28.8592361852886,29.8379489392154,30.8166616931422,31.7953744470691,32.7740872009959,
33.7527999549228,34.7315127088496,35.7102254627764,36.6889382167033,37.6676509706301,
38.646363724557,39.6250764784838,40.6037892324106,41.5825019863375),
 .UNSPECIFIED.);
#83=B_SPLINE_SURFACE_WITH_KNOTS('',3,3,((#8785,#8786,#8787,#8788,#8789,
#8790,#8791,#8792,#8793,#8794,#8795,#8796,#8797,#8798,#8799,#8800,#8801,
#8802,#8803,#8804,#8805,#8806,#8807,#8808,#8809,#8810,#8811,#8812,#8813,
#8814,#8815,#8816,#8817,#8818,#8819,#8820,#8821),(#8822,#8823,#8824,#8825,
#8826,#8827,#8828,#8829,#8830,#8831,#8832,#8833,#8834,#8835,#8836,#8837,
#8838,#8839,#8840,#8841,#8842,#8843,#8844,#8845,#8846,#8847,#8848,#8849,
#8850,#8851,#8852,#8853,#8854,#8855,#8856,#8857,#8858),(#8859,#8860,#8861,
#8862,#8863,#8864,#8865,#8866,#8867,#8868,#8869,#8870,#8871,#8872,#8873,
#8874,#8875,#8876,#8877,#8878,#8879,#8880,#8881,#8882,#8883,#8884,#8885,
#8886,#8887,#8888,#8889,#8890,#8891,#8892,#8893,#8894,#8895),(#8896,#8897,
#8898,#8899,#8900,#8901,#8902,#8903,#8904,#8905,#8906,#8907,#8908,#8909,
#8910,#8911,#8912,#8913,#8914,#8915,#8916,#8917,#8918,#8919,#8920,#8921,
#8922,#8923,#8924,#8925,#8926,#8927,#8928,#8929,#8930,#8931,#8932)),
 .UNSPECIFIED.,.F.,.F.,.F.,(4,4),(4,1,1,1,1,1,1,1,1,1,1,1,1,1,1,1,1,1,1,
1,1,1,1,1,1,1,1,1,1,1,1,1,1,1,4),(0.,0.0296469363228873),(11.6151336144497,
12.5938463683765,13.5725591223033,14.5512718762302,15.529984630157,16.5086973840839,
17.4874101380107,18.4661228919375,19.4448356458644,20.4235483997912,21.4022611537181,
22.3809739076449,23.3596866615717,24.3383994154986,25.3171121694254,26.2958249233523,
27.2745376772791,28.2532504312059,29.2319631851328,30.2106759390596,31.1893886929865,
32.1681014469133,33.1468142008401,34.125526954767,35.1042397086938,36.0829524626207,
37.0616652165475,38.0403779704743,39.0190907244012,39.997803478328,40.9765162322549,
41.9552289861817,42.9339417401085,43.9126544940354,44.8913672479622),
 .UNSPECIFIED.);
#132=B_SPLINE_CURVE_WITH_KNOTS('',3,(#8022,#8023,#8024,#8025,#8026,#8027,
#8028,#8029,#8030,#8031),.UNSPECIFIED.,.F.,.F.,(4,3,3,4),(-4.0928296534993,
-3.91485101570736,-2.93613826178052,-2.06974660785394),.UNSPECIFIED.);
#133=B_SPLINE_CURVE_WITH_KNOTS('',3,(#8034,#8035,#8036,#8037,#8038,#8039,
#8040),.UNSPECIFIED.,.F.,.F.,(4,3,4),(0.,0.97871275392684,1.11850960794444),
 .UNSPECIFIED.);
#134=B_SPLINE_CURVE_WITH_KNOTS('',3,(#8045,#8046,#8047,#8048,#8049,#8050,
#8051,#8052,#8053,#8054,#8055,#8056,#8057,#8058,#8059,#8060,#8061,#8062,
#8063,#8064,#8065,#8066),.UNSPECIFIED.,.F.,.F.,(4,3,3,3,3,3,3,4),(-10.3760149606789,
-9.7871275392684,-8.80841478534156,-7.82970203141472,-6.85098927748787,
-5.87227652356104,-4.8935637696342,-4.0928296534993),.UNSPECIFIED.);
#135=B_SPLINE_CURVE_WITH_KNOTS('',3,(#8067,#8068,#8069,#8070,#8071,#8072,
#8073,#8074,#8075,#8076,#8077,#8078,#8079,#8080,#8081,#8082,#8083,#8084,
#8085,#8086,#8087,#8088),.UNSPECIFIED.,.F.,.F.,(4,3,3,3,3,3,3,4),(1.11850960794444,
1.95742550785368,2.93613826178052,3.91485101570736,4.8935637696342,5.87227652356104,
6.85098927748788,7.40169491512403),.UNSPECIFIED.);
#136=B_SPLINE_CURVE_WITH_KNOTS('',3,(#8093,#8094,#8095,#8096,#8097,#8098,
#8099,#8100,#8101,#8102,#8103,#8104,#8105,#8106,#8107,#8108,#8109,#8110,
#8111,#8112,#8113,#8114,#8115,#8116,#8117),.UNSPECIFIED.,.F.,.F.,(4,3,3,
3,3,3,3,3,4),(-16.6592002678585,-16.6381168167563,-15.6594040628294,-14.6806913089026,
-13.7019785549758,-12.7232658010489,-11.7445530471221,-10.7658402931952,
-10.3760149606789),.UNSPECIFIED.);
#137=B_SPLINE_CURVE_WITH_KNOTS('',3,(#8118,#8119,#8120,#8121,#8122,#8123,
#8124,#8125,#8126,#8127,#8128,#8129,#8130,#8131,#8132,#8133,#8134,#8135,
#8136,#8137,#8138,#8139),.UNSPECIFIED.,.F.,.F.,(4,3,3,3,3,3,3,4),(7.40169491512403,
7.82970203141472,8.80841478534156,9.78712753926839,10.7658402931952,11.7445530471221,
12.7232658010489,13.6848802223036),.UNSPECIFIED.);
#138=B_SPLINE_CURVE_WITH_KNOTS('',3,(#8144,#8145,#8146,#8147,#8148,#8149,
#8150,#8151,#8152,#8153,#8154,#8155,#8156,#8157,#8158,#8159,#8160,#8161,
#8162,#8163,#8164,#8165),.UNSPECIFIED.,.F.,.F.,(4,3,3,3,3,3,3,4),(-22.9423855750381,
-22.5103933403173,-21.5316805863905,-20.5529678324636,-19.5742550785368,
-18.59554232461,-17.6168295706831,-16.6592002678585),.UNSPECIFIED.);
#139=B_SPLINE_CURVE_WITH_KNOTS('',3,(#8166,#8167,#8168,#8169,#8170,#8171,
#8172,#8173,#8174,#8175,#8176,#8177,#8178,#8179,#8180,#8181,#8182,#8183,
#8184,#8185,#8186,#8187,#8188,#8189,#8190),.UNSPECIFIED.,.F.,.F.,(4,3,3,
3,3,3,3,3,4),(13.6848802223036,13.7019785549758,14.6806913089026,15.6594040628294,
16.6381168167563,17.6168295706831,18.5955423246099,19.5742550785368,19.9680655294832),
 .UNSPECIFIED.);
#140=B_SPLINE_CURVE_WITH_KNOTS('',3,(#8195,#8196,#8197,#8198,#8199,#8200,
#8201,#8202,#8203,#8204,#8205,#8206,#8207,#8208,#8209,#8210,#8211,#8212,
#8213,#8214,#8215,#8216),.UNSPECIFIED.,.F.,.F.,(4,3,3,3,3,3,3,4),(-29.2255708822176,
-28.3826698638783,-27.4039571099515,-26.4252443560247,-25.4465316020978,
-24.467818848171,-23.4891060942441,-22.9423855750381),.UNSPECIFIED.);
#141=B_SPLINE_CURVE_WITH_KNOTS('',3,(#8217,#8218,#8219,#8220,#8221,#8222,
#8223,#8224,#8225,#8226,#8227,#8228,#8229,#8230,#8231,#8232,#8233,#8234,
#8235,#8236,#8237,#8238),.UNSPECIFIED.,.F.,.F.,(4,3,3,3,3,3,3,4),(19.9680655294832,
20.5529678324636,21.5316805863905,22.5103933403173,23.4891060942441,24.467818848171,
25.4465316020978,26.2512508366628),.UNSPECIFIED.);
#142=B_SPLINE_CURVE_WITH_KNOTS('',3,(#8244,#8245,#8246,#8247,#8248,#8249),
 .UNSPECIFIED.,.F.,.F.,(4,1,1,4),(40.8407044966673,40.9765162322549,41.9552289861817,
42.8216206401083),.UNSPECIFIED.);
#143=B_SPLINE_CURVE_WITH_KNOTS('',3,(#8252,#8253,#8254,#8255),
 .UNSPECIFIED.,.F.,.F.,(4,4),(40.8407044966673,41.5825019863375),
 .UNSPECIFIED.);
#144=B_SPLINE_CURVE_WITH_KNOTS('',3,(#8260,#8261,#8262,#8263,#8264,#8265,
#8266,#8267,#8268,#8269),.UNSPECIFIED.,.F.,.F.,(4,1,1,1,1,1,1,4),(34.5575191894877,
35.1042397086938,36.0829524626207,37.0616652165475,38.0403779704743,39.0190907244012,
39.997803478328,40.8407044966673),.UNSPECIFIED.);
#145=B_SPLINE_CURVE_WITH_KNOTS('',3,(#8270,#8271,#8272,#8273,#8274,#8275,
#8276,#8277,#8278,#8279,#8280),.UNSPECIFIED.,.F.,.F.,(4,1,1,1,1,1,1,1,4),
(34.5575191894877,34.7315127088496,35.7102254627764,36.6889382167033,37.6676509706301,
38.646363724557,39.6250764784838,40.6037892324106,40.8407044966673),
 .UNSPECIFIED.);
#146=B_SPLINE_CURVE_WITH_KNOTS('',3,(#8285,#8286,#8287,#8288,#8289,#8290,
#8291,#8292,#8293,#8294),.UNSPECIFIED.,.F.,.F.,(4,1,1,1,1,1,1,4),(28.2743338823081,
29.2319631851328,30.2106759390596,31.1893886929865,32.1681014469133,33.1468142008401,
34.125526954767,34.5575191894877),.UNSPECIFIED.);
#147=B_SPLINE_CURVE_WITH_KNOTS('',3,(#8295,#8296,#8297,#8298,#8299,#8300,
#8301,#8302,#8303,#8304),.UNSPECIFIED.,.F.,.F.,(4,1,1,1,1,1,1,4),(28.2743338823081,
28.8592361852886,29.8379489392154,30.8166616931422,31.7953744470691,32.7740872009959,
33.7527999549228,34.5575191894877),.UNSPECIFIED.);
#148=B_SPLINE_CURVE_WITH_KNOTS('',3,(#8309,#8310,#8311,#8312,#8313,#8314,
#8315,#8316,#8317,#8318,#8319),.UNSPECIFIED.,.F.,.F.,(4,1,1,1,1,1,1,1,4),
(21.9911485751285,22.3809739076449,23.3596866615717,24.3383994154986,25.3171121694254,
26.2958249233523,27.2745376772791,28.2532504312059,28.2743338823081),
 .UNSPECIFIED.);
#149=B_SPLINE_CURVE_WITH_KNOTS('',3,(#8320,#8321,#8322,#8323,#8324,#8325,
#8326,#8327,#8328,#8329,#8330),.UNSPECIFIED.,.F.,.F.,(4,1,1,1,1,1,1,1,4),
(21.9911485751285,22.0082469078007,22.9869596617275,23.9656724156544,24.9443851695812,
25.923097923508,26.9018106774349,27.8805234313617,28.2743338823081),
 .UNSPECIFIED.);
#150=B_SPLINE_CURVE_WITH_KNOTS('',3,(#8335,#8336,#8337,#8338,#8339,#8340,
#8341,#8342,#8343,#8344),.UNSPECIFIED.,.F.,.F.,(4,1,1,1,1,1,1,4),(15.707963267949,
16.5086973840839,17.4874101380107,18.4661228919375,19.4448356458644,20.4235483997912,
21.4022611537181,21.9911485751285),.UNSPECIFIED.);
#151=B_SPLINE_CURVE_WITH_KNOTS('',3,(#8345,#8346,#8347,#8348,#8349,#8350,
#8351,#8352,#8353,#8354),.UNSPECIFIED.,.F.,.F.,(4,1,1,1,1,1,1,4),(15.707963267949,
16.1359703842396,17.1146831381665,18.0933958920933,19.0721086460202,20.050821399947,
21.0295341538738,21.9911485751285),.UNSPECIFIED.);
#152=B_SPLINE_CURVE_WITH_KNOTS('',3,(#8504,#8505,#8506,#8507,#8508,#8509,
#8510,#8511,#8512,#8513,#8514,#8515,#8516,#8517,#8518,#8519,#8520,#8521,
#8522,#8523,#8524,#8525,#8526,#8527,#8528,#8529,#8530,#8531,#8532,#8533,
#8534,#8535,#8536,#8537,#8538,#8539,#8540,#8541,#8542,#8543,#8544,#8545,
#8546,#8547,#8548,#8549,#8550,#8551,#8552,#8553,#8554,#8555,#8556,#8557,
#8558,#8559,#8560,#8561,#8562,#8563,#8564,#8565,#8566,#8567,#8568,#8569,
#8570,#8571,#8572,#8573,#8574,#8575,#8576,#8577,#8578,#8579,#8580,#8581,
#8582,#8583,#8584,#8585),.UNSPECIFIED.,.F.,.F.,(4,3,3,3,3,3,3,3,3,3,3,3,
3,3,3,3,3,3,3,3,3,3,3,3,3,3,3,4),(-0.2263798216096,-0.212781296643935,-0.198764954499484,
-0.194348244024141,-0.19103137880398,-0.176141645981783,-0.166705260170101,
-0.163156832255381,-0.160273007739967,-0.145367395677056,-0.131314184979161,
-0.123648278606451,-0.12009892302652,-0.117708066911632,-0.104064816705108,
-0.100650559488324,-0.0880692395522834,-0.0819584633849732,-0.0783172232476268,
-0.0758731537810384,-0.0623358096117628,-0.0488821760013612,-0.0427719040011911,
-0.0392847357791446,-0.036186254561982,-0.0232691518627682,-0.0108090455882997,
0.),.UNSPECIFIED.);
#153=B_SPLINE_CURVE_WITH_KNOTS('',3,(#8586,#8587,#8588,#8589,#8590,#8591,
#8592,#8593,#8594,#8595,#8596,#8597,#8598,#8599,#8600,#8601,#8602,#8603,
#8604),.UNSPECIFIED.,.F.,.F.,(4,3,3,3,3,3,4),(26.2512508366628,26.4252443560247,
27.4039571099515,28.3826698638783,29.3613826178052,30.340095371732,31.2064870256586),
 .UNSPECIFIED.);
#154=B_SPLINE_CURVE_WITH_KNOTS('',3,(#8606,#8607,#8608,#8609,#8610,#8611,
#8612,#8613,#8614,#8615,#8616,#8617,#8618,#8619,#8620,#8621,#8622,#8623,
#8624,#8625,#8626,#8627,#8628,#8629,#8630,#8631,#8632,#8633,#8634,#8635,
#8636,#8637,#8638,#8639,#8640,#8641,#8642,#8643,#8644,#8645,#8646,#8647,
#8648,#8649,#8650,#8651,#8652,#8653,#8654,#8655,#8656,#8657,#8658,#8659,
#8660,#8661,#8662,#8663,#8664,#8665,#8666,#8667,#8668,#8669,#8670,#8671,
#8672,#8673,#8674,#8675,#8676,#8677,#8678),.UNSPECIFIED.,.F.,.F.,(4,3,3,
3,3,3,3,3,3,3,3,3,3,3,3,3,3,3,3,3,3,3,3,3,4),(-0.227523845437315,-0.216531207791372,
-0.203444509678888,-0.19917031778805,-0.186104896969351,-0.177062709219988,
-0.174032359669319,-0.160576649118607,-0.146770239359644,-0.138606747212735,
-0.134066956125942,-0.131712797600661,-0.117458517615624,-0.114116270772009,
-0.0998517369255078,-0.0931579911241419,-0.0906511125980258,-0.0764034745604488,
-0.0618085878200202,-0.0535532362928206,-0.0474979476179205,-0.0444986209948431,
-0.0293718149083609,-0.0143385875077465,0.),.UNSPECIFIED.);
#155=B_SPLINE_CURVE_WITH_KNOTS('',3,(#8679,#8680,#8681,#8682,#8683,#8684,
#8685,#8686,#8687),.UNSPECIFIED.,.F.,.F.,(4,1,1,1,1,1,4),(10.3760149606789,
11.2424066146055,12.2211193685323,13.1998321224591,14.178544876386,15.1572576303128,
15.707963267949),.UNSPECIFIED.);
#156=B_SPLINE_CURVE_WITH_KNOTS('',3,(#8693,#8694,#8695,#8696,#8697,#8698,
#8699,#8700,#8701,#8702,#8703,#8704,#8705,#8706,#8707,#8708,#8709,#8710,
#8711,#8712,#8713,#8714,#8715,#8716,#8717,#8718,#8719,#8720,#8721,#8722,
#8723,#8724,#8725,#8726,#8727,#8728,#8729,#8730,#8731,#8732,#8733,#8734,
#8735,#8736,#8737,#8738,#8739,#8740,#8741,#8742,#8743,#8744,#8745,#8746,
#8747,#8748,#8749,#8750,#8751,#8752,#8753,#8754,#8755,#8756,#8757,#8758,
#8759,#8760,#8761,#8762,#8763,#8764,#8765,#8766,#8767,#8768,#8769,#8770,
#8771,#8772,#8773,#8774),.UNSPECIFIED.,.F.,.F.,(4,3,3,3,3,3,3,3,3,3,3,3,
3,3,3,3,3,3,3,3,3,3,3,3,3,3,3,4),(-0.226379821609601,-0.212781296643936,
-0.198764954499484,-0.194348229390083,-0.191031373550795,-0.176141640284406,
-0.166705255184896,-0.163156771711209,-0.160272993847505,-0.14536738525771,
-0.131314163159309,-0.123648262241563,-0.120098829594509,-0.117707924800541,
-0.10406466589718,-0.100650559488325,-0.0880692395522841,-0.0819584595318643,
-0.0783172123161553,-0.0758731354163763,-0.062335788826532,-0.0488821638473745,
-0.0427718933664527,-0.0392847312763369,-0.0361862533404839,-0.0232691611782643,
-0.0108090724668815,0.),.UNSPECIFIED.);
#157=B_SPLINE_CURVE_WITH_KNOTS('',3,(#8777,#8778,#8779,#8780,#8781,#8782,
#8783,#8784),.UNSPECIFIED.,.F.,.F.,(4,1,1,1,1,4),(11.6151336144497,12.5938463683765,
13.5725591223033,14.5512718762302,15.529984630157,15.707963267949),
 .UNSPECIFIED.);
#158=B_SPLINE_CURVE_WITH_KNOTS('',3,(#8934,#8935,#8936,#8937,#8938,#8939,
#8940,#8941,#8942,#8943,#8944,#8945,#8946,#8947,#8948,#8949,#8950,#8951,
#8952,#8953,#8954,#8955,#8956,#8957,#8958,#8959,#8960,#8961,#8962,#8963,
#8964,#8965,#8966,#8967,#8968,#8969,#8970,#8971,#8972,#8973,#8974,#8975,
#8976,#8977,#8978,#8979,#8980,#8981,#8982,#8983,#8984,#8985,#8986,#8987,
#8988,#8989,#8990,#8991,#8992,#8993,#8994,#8995,#8996,#8997,#8998,#8999,
#9000,#9001,#9002,#9003,#9004,#9005,#9006),.UNSPECIFIED.,.F.,.F.,(4,3,3,
3,3,3,3,3,3,3,3,3,3,3,3,3,3,3,3,3,3,3,3,3,4),(-0.227523845437336,-0.216531207791394,
-0.203444511100821,-0.199170316873814,-0.186104887794658,-0.177062692209482,
-0.174032347803623,-0.160576629297939,-0.146770219866148,-0.138606732592615,
-0.134066934232983,-0.13171277086904,-0.117458491234212,-0.114116270772017,
-0.0998517369255152,-0.0931579924169406,-0.0906511134895252,-0.0764034708381965,
-0.0618085789631532,-0.0535532325040275,-0.0474979353490834,-0.0444986239739673,
-0.0293718142479027,-0.0143385961848834,0.),.UNSPECIFIED.);
#159=B_SPLINE_CURVE_WITH_KNOTS('',3,(#9007,#9008,#9009,#9010,#9011,#9012,
#9013,#9014,#9015,#9016,#9017,#9018,#9019,#9020,#9021,#9022),
 .UNSPECIFIED.,.F.,.F.,(4,3,3,3,3,4),(-33.2762336335125,-32.2975208795857,
-31.3188081256589,-30.340095371732,-29.3613826178052,-29.2255708822176),
 .UNSPECIFIED.);
#242=SHAPE_REPRESENTATION_RELATIONSHIP('SRR','None',#11485,#254);
#254=ADVANCED_BREP_SHAPE_REPRESENTATION('',(#278),#11424);
#266=STYLED_ITEM('',(#11616),#278);
#278=MANIFOLD_SOLID_BREP('Body1',#4467);
#307=FACE_BOUND('',#966,.T.);
#308=FACE_BOUND('',#976,.T.);
#309=FACE_BOUND('',#981,.T.);
#380=PLANE('',#4856);
#381=PLANE('',#4861);
#382=PLANE('',#4862);
#383=PLANE('',#4863);
#384=PLANE('',#4869);
#385=PLANE('',#4871);
#386=PLANE('',#4873);
#387=PLANE('',#4875);
#388=PLANE('',#4877);
#389=PLANE('',#4879);
#390=PLANE('',#4881);
#391=PLANE('',#4888);
#392=PLANE('',#4893);
#469=CYLINDRICAL_SURFACE('',#4844,1.215);
#470=CYLINDRICAL_SURFACE('',#4846,1.215);
#471=CYLINDRICAL_SURFACE('',#4847,1.215);
#472=CYLINDRICAL_SURFACE('',#4848,1.215);
#473=CYLINDRICAL_SURFACE('',#4849,1.215);
#474=CYLINDRICAL_SURFACE('',#4850,0.95825);
#475=CYLINDRICAL_SURFACE('',#4852,0.95825);
#476=CYLINDRICAL_SURFACE('',#4853,0.95825);
#477=CYLINDRICAL_SURFACE('',#4854,0.95825);
#478=CYLINDRICAL_SURFACE('',#4855,0.95825);
#479=CYLINDRICAL_SURFACE('',#4860,0.95825);
#480=CYLINDRICAL_SURFACE('',#4867,2.25);
#481=CYLINDRICAL_SURFACE('',#4891,1.215);
#482=CYLINDRICAL_SURFACE('',#4895,2.25);
#483=CYLINDRICAL_SURFACE('',#4896,1.5);
#658=FACE_OUTER_BOUND('',#949,.T.);
#659=FACE_OUTER_BOUND('',#950,.T.);
#660=FACE_OUTER_BOUND('',#951,.T.);
#661=FACE_OUTER_BOUND('',#952,.T.);
#662=FACE_OUTER_BOUND('',#953,.T.);
#663=FACE_OUTER_BOUND('',#954,.T.);
#664=FACE_OUTER_BOUND('',#955,.T.);
#665=FACE_OUTER_BOUND('',#956,.T.);
#666=FACE_OUTER_BOUND('',#957,.T.);
#667=FACE_OUTER_BOUND('',#958,.T.);
#668=FACE_OUTER_BOUND('',#959,.T.);
#669=FACE_OUTER_BOUND('',#960,.T.);
#670=FACE_OUTER_BOUND('',#961,.T.);
#671=FACE_OUTER_BOUND('',#962,.T.);
#672=FACE_OUTER_BOUND('',#963,.T.);
#673=FACE_OUTER_BOUND('',#964,.T.);
#674=FACE_OUTER_BOUND('',#965,.T.);
#675=FACE_OUTER_BOUND('',#967,.T.);
#676=FACE_OUTER_BOUND('',#968,.T.);
#677=FACE_OUTER_BOUND('',#969,.T.);
#678=FACE_OUTER_BOUND('',#970,.T.);
#679=FACE_OUTER_BOUND('',#971,.T.);
#680=FACE_OUTER_BOUND('',#972,.T.);
#681=FACE_OUTER_BOUND('',#973,.T.);
#682=FACE_OUTER_BOUND('',#974,.T.);
#683=FACE_OUTER_BOUND('',#975,.T.);
#684=FACE_OUTER_BOUND('',#977,.T.);
#685=FACE_OUTER_BOUND('',#978,.T.);
#686=FACE_OUTER_BOUND('',#979,.T.);
#687=FACE_OUTER_BOUND('',#980,.T.);
#688=FACE_OUTER_BOUND('',#982,.T.);
#689=FACE_OUTER_BOUND('',#983,.T.);
#949=EDGE_LOOP('',(#3473,#3474,#3475,#3476));
#950=EDGE_LOOP('',(#3477,#3478,#3479,#3480));
#951=EDGE_LOOP('',(#3481,#3482,#3483,#3484));
#952=EDGE_LOOP('',(#3485,#3486,#3487,#3488));
#953=EDGE_LOOP('',(#3489,#3490,#3491,#3492));
#954=EDGE_LOOP('',(#3493,#3494,#3495,#3496));
#955=EDGE_LOOP('',(#3497,#3498,#3499,#3500));
#956=EDGE_LOOP('',(#3501,#3502,#3503,#3504));
#957=EDGE_LOOP('',(#3505,#3506,#3507,#3508));
#958=EDGE_LOOP('',(#3509,#3510,#3511,#3512));
#959=EDGE_LOOP('',(#3513,#3514,#3515,#3516,#3517,#3518,#3519,#3520,#3521,
#3522,#3523,#3524,#3525,#3526));
#960=EDGE_LOOP('',(#3527,#3528,#3529,#3530,#3531));
#961=EDGE_LOOP('',(#3532,#3533,#3534,#3535));
#962=EDGE_LOOP('',(#3536,#3537,#3538,#3539,#3540,#3541,#3542,#3543,#3544,
#3545,#3546,#3547,#3548,#3549));
#963=EDGE_LOOP('',(#3550,#3551,#3552,#3553));
#964=EDGE_LOOP('',(#3554,#3555,#3556,#3557));
#965=EDGE_LOOP('',(#3558,#3559,#3560,#3561));
#966=EDGE_LOOP('',(#3562));
#967=EDGE_LOOP('',(#3563,#3564,#3565,#3566));
#968=EDGE_LOOP('',(#3567,#3568,#3569,#3570));
#969=EDGE_LOOP('',(#3571,#3572,#3573,#3574));
#970=EDGE_LOOP('',(#3575,#3576,#3577,#3578));
#971=EDGE_LOOP('',(#3579,#3580,#3581,#3582));
#972=EDGE_LOOP('',(#3583,#3584,#3585,#3586));
#973=EDGE_LOOP('',(#3587,#3588,#3589,#3590));
#974=EDGE_LOOP('',(#3591,#3592,#3593,#3594,#3595,#3596));
#975=EDGE_LOOP('',(#3597,#3598,#3599,#3600,#3601,#3602,#3603));
#976=EDGE_LOOP('',(#3604,#3605,#3606,#3607,#3608,#3609));
#977=EDGE_LOOP('',(#3610));
#978=EDGE_LOOP('',(#3611,#3612,#3613,#3614,#3615,#3616));
#979=EDGE_LOOP('',(#3617,#3618,#3619,#3620));
#980=EDGE_LOOP('',(#3621,#3622,#3623,#3624));
#981=EDGE_LOOP('',(#3625,#3626,#3627,#3628));
#982=EDGE_LOOP('',(#3629,#3630,#3631,#3632));
#983=EDGE_LOOP('',(#3633,#3634,#3635,#3636,#3637,#3638));
#1233=LINE('',#8020,#1523);
#1234=LINE('',#8044,#1524);
#1235=LINE('',#8092,#1525);
#1236=LINE('',#8143,#1526);
#1237=LINE('',#8194,#1527);
#1238=LINE('',#8242,#1528);
#1239=LINE('',#8259,#1529);
#1240=LINE('',#8284,#1530);
#1241=LINE('',#8308,#1531);
#1242=LINE('',#8334,#1532);
#1243=LINE('',#9026,#1533);
#1244=LINE('',#9028,#1534);
#1245=LINE('',#9030,#1535);
#1246=LINE('',#9031,#1536);
#1247=LINE('',#9035,#1537);
#1248=LINE('',#9037,#1538);
#1249=LINE('',#9039,#1539);
#1250=LINE('',#9040,#1540);
#1251=LINE('',#9053,#1541);
#1252=LINE('',#9055,#1542);
#1253=LINE('',#9056,#1543);
#1254=LINE('',#9061,#1544);
#1255=LINE('',#9062,#1545);
#1256=LINE('',#9067,#1546);
#1257=LINE('',#9068,#1547);
#1258=LINE('',#9073,#1548);
#1259=LINE('',#9074,#1549);
#1260=LINE('',#9079,#1550);
#1261=LINE('',#9080,#1551);
#1262=LINE('',#9083,#1552);
#1263=LINE('',#9100,#1553);
#1264=LINE('',#9107,#1554);
#1523=VECTOR('',#5693,1.25);
#1524=VECTOR('',#5698,1.25);
#1525=VECTOR('',#5701,1.25);
#1526=VECTOR('',#5704,1.25);
#1527=VECTOR('',#5707,1.25);
#1528=VECTOR('',#5710,0.95825);
#1529=VECTOR('',#5715,0.95825);
#1530=VECTOR('',#5718,0.95825);
#1531=VECTOR('',#5721,0.95825);
#1532=VECTOR('',#5724,0.95825);
#1533=VECTOR('',#5737,10.);
#1534=VECTOR('',#5738,10.);
#1535=VECTOR('',#5739,10.);
#1536=VECTOR('',#5740,10.);
#1537=VECTOR('',#5743,10.);
#1538=VECTOR('',#5744,10.);
#1539=VECTOR('',#5745,10.);
#1540=VECTOR('',#5746,10.);
#1541=VECTOR('',#5763,10.);
#1542=VECTOR('',#5764,10.);
#1543=VECTOR('',#5765,10.);
#1544=VECTOR('',#5770,10.);
#1545=VECTOR('',#5771,10.);
#1546=VECTOR('',#5776,10.);
#1547=VECTOR('',#5777,10.);
#1548=VECTOR('',#5782,10.);
#1549=VECTOR('',#5783,10.);
#1550=VECTOR('',#5788,10.);
#1551=VECTOR('',#5789,10.);
#1552=VECTOR('',#5794,10.);
#1553=VECTOR('',#5815,1.15);
#1554=VECTOR('',#5828,1.5);
#1781=CIRCLE('',#4845,1.215);
#1782=CIRCLE('',#4851,0.95825);
#1783=CIRCLE('',#4857,1.215);
#1784=CIRCLE('',#4858,1.215);
#1785=CIRCLE('',#4859,0.95825);
#1786=CIRCLE('',#4864,2.25);
#1787=CIRCLE('',#4865,2.25);
#1788=CIRCLE('',#4866,1.5);
#1789=CIRCLE('',#4868,2.25);
#1790=CIRCLE('',#4870,2.64575131106459);
#1791=CIRCLE('',#4872,2.64575131106459);
#1792=CIRCLE('',#4874,2.64575131106459);
#1793=CIRCLE('',#4876,2.64575131106459);
#1794=CIRCLE('',#4878,2.64575131106459);
#1795=CIRCLE('',#4880,2.64575131106459);
#1796=CIRCLE('',#4883,1.5);
#1797=CIRCLE('',#4884,1.5);
#1798=CIRCLE('',#4885,2.75);
#1799=CIRCLE('',#4886,1.5);
#1800=CIRCLE('',#4887,2.75);
#1801=CIRCLE('',#4889,1.05);
#1802=CIRCLE('',#4892,1.215);
#1803=CIRCLE('',#4894,2.25);
#2047=VERTEX_POINT('',#8018);
#2048=VERTEX_POINT('',#8019);
#2049=VERTEX_POINT('',#8021);
#2050=VERTEX_POINT('',#8032);
#2051=VERTEX_POINT('',#8042);
#2052=VERTEX_POINT('',#8043);
#2053=VERTEX_POINT('',#8090);
#2054=VERTEX_POINT('',#8091);
#2055=VERTEX_POINT('',#8141);
#2056=VERTEX_POINT('',#8142);
#2057=VERTEX_POINT('',#8192);
#2058=VERTEX_POINT('',#8193);
#2059=VERTEX_POINT('',#8240);
#2060=VERTEX_POINT('',#8241);
#2061=VERTEX_POINT('',#8243);
#2062=VERTEX_POINT('',#8250);
#2063=VERTEX_POINT('',#8257);
#2064=VERTEX_POINT('',#8258);
#2065=VERTEX_POINT('',#8282);
#2066=VERTEX_POINT('',#8283);
#2067=VERTEX_POINT('',#8306);
#2068=VERTEX_POINT('',#8307);
#2069=VERTEX_POINT('',#8332);
#2070=VERTEX_POINT('',#8333);
#2071=VERTEX_POINT('',#8503);
#2072=VERTEX_POINT('',#8605);
#2073=VERTEX_POINT('',#8689);
#2074=VERTEX_POINT('',#8692);
#2075=VERTEX_POINT('',#8933);
#2076=VERTEX_POINT('',#9024);
#2077=VERTEX_POINT('',#9025);
#2078=VERTEX_POINT('',#9027);
#2079=VERTEX_POINT('',#9029);
#2080=VERTEX_POINT('',#9033);
#2081=VERTEX_POINT('',#9034);
#2082=VERTEX_POINT('',#9036);
#2083=VERTEX_POINT('',#9038);
#2084=VERTEX_POINT('',#9044);
#2085=VERTEX_POINT('',#9049);
#2086=VERTEX_POINT('',#9050);
#2087=VERTEX_POINT('',#9052);
#2088=VERTEX_POINT('',#9054);
#2089=VERTEX_POINT('',#9058);
#2090=VERTEX_POINT('',#9060);
#2091=VERTEX_POINT('',#9064);
#2092=VERTEX_POINT('',#9066);
#2093=VERTEX_POINT('',#9070);
#2094=VERTEX_POINT('',#9072);
#2095=VERTEX_POINT('',#9076);
#2096=VERTEX_POINT('',#9078);
#2097=VERTEX_POINT('',#9086);
#2098=VERTEX_POINT('',#9087);
#2099=VERTEX_POINT('',#9089);
#2100=VERTEX_POINT('',#9091);
#2101=VERTEX_POINT('',#9094);
#2102=VERTEX_POINT('',#9097);
#2554=EDGE_CURVE('',#2047,#2048,#1233,.T.);
#2555=EDGE_CURVE('',#2047,#2049,#132,.T.);
#2556=EDGE_CURVE('',#2049,#2050,#1781,.T.);
#2557=EDGE_CURVE('',#2050,#2048,#133,.T.);
#2558=EDGE_CURVE('',#2051,#2052,#1234,.T.);
#2559=EDGE_CURVE('',#2051,#2047,#134,.T.);
#2560=EDGE_CURVE('',#2048,#2052,#135,.T.);
#2561=EDGE_CURVE('',#2053,#2054,#1235,.T.);
#2562=EDGE_CURVE('',#2053,#2051,#136,.T.);
#2563=EDGE_CURVE('',#2052,#2054,#137,.T.);
#2564=EDGE_CURVE('',#2055,#2056,#1236,.T.);
#2565=EDGE_CURVE('',#2055,#2053,#138,.T.);
#2566=EDGE_CURVE('',#2054,#2056,#139,.T.);
#2567=EDGE_CURVE('',#2057,#2058,#1237,.T.);
#2568=EDGE_CURVE('',#2057,#2055,#140,.T.);
#2569=EDGE_CURVE('',#2056,#2058,#141,.T.);
#2570=EDGE_CURVE('',#2059,#2060,#1238,.T.);
#2571=EDGE_CURVE('',#2059,#2061,#142,.T.);
#2572=EDGE_CURVE('',#2062,#2061,#1782,.T.);
#2573=EDGE_CURVE('',#2060,#2062,#143,.T.);
#2574=EDGE_CURVE('',#2063,#2064,#1239,.T.);
#2575=EDGE_CURVE('',#2063,#2059,#144,.T.);
#2576=EDGE_CURVE('',#2064,#2060,#145,.T.);
#2577=EDGE_CURVE('',#2065,#2066,#1240,.T.);
#2578=EDGE_CURVE('',#2065,#2063,#146,.T.);
#2579=EDGE_CURVE('',#2066,#2064,#147,.T.);
#2580=EDGE_CURVE('',#2067,#2068,#1241,.T.);
#2581=EDGE_CURVE('',#2067,#2065,#148,.T.);
#2582=EDGE_CURVE('',#2068,#2066,#149,.T.);
#2583=EDGE_CURVE('',#2069,#2070,#1242,.T.);
#2584=EDGE_CURVE('',#2069,#2067,#150,.T.);
#2585=EDGE_CURVE('',#2070,#2068,#151,.T.);
#2586=EDGE_CURVE('',#2071,#2062,#152,.T.);
#2587=EDGE_CURVE('',#2058,#2071,#153,.T.);
#2588=EDGE_CURVE('',#2072,#2050,#154,.T.);
#2589=EDGE_CURVE('',#2072,#2070,#155,.T.);
#2590=EDGE_CURVE('',#2050,#2073,#1783,.T.);
#2591=EDGE_CURVE('',#2073,#2049,#1784,.T.);
#2592=EDGE_CURVE('',#2049,#2074,#156,.T.);
#2593=EDGE_CURVE('',#2074,#2072,#1785,.T.);
#2594=EDGE_CURVE('',#2074,#2069,#157,.T.);
#2595=EDGE_CURVE('',#2061,#2075,#158,.T.);
#2596=EDGE_CURVE('',#2075,#2057,#159,.T.);
#2597=EDGE_CURVE('',#2076,#2077,#1243,.T.);
#2598=EDGE_CURVE('',#2078,#2076,#1244,.T.);
#2599=EDGE_CURVE('',#2079,#2078,#1245,.T.);
#2600=EDGE_CURVE('',#2077,#2079,#1246,.T.);
#2601=EDGE_CURVE('',#2080,#2081,#1247,.T.);
#2602=EDGE_CURVE('',#2082,#2080,#1248,.T.);
#2603=EDGE_CURVE('',#2083,#2082,#1249,.T.);
#2604=EDGE_CURVE('',#2081,#2083,#1250,.T.);
#2605=EDGE_CURVE('',#2079,#2081,#1786,.T.);
#2606=EDGE_CURVE('',#2083,#2077,#1787,.T.);
#2607=EDGE_CURVE('',#2084,#2084,#1788,.T.);
#2608=EDGE_CURVE('',#2078,#2080,#1789,.T.);
#2609=EDGE_CURVE('',#2085,#2086,#1790,.T.);
#2610=EDGE_CURVE('',#2085,#2087,#1251,.T.);
#2611=EDGE_CURVE('',#2087,#2088,#1252,.T.);
#2612=EDGE_CURVE('',#2086,#2088,#1253,.T.);
#2613=EDGE_CURVE('',#2086,#2089,#1791,.T.);
#2614=EDGE_CURVE('',#2088,#2090,#1254,.T.);
#2615=EDGE_CURVE('',#2089,#2090,#1255,.T.);
#2616=EDGE_CURVE('',#2089,#2091,#1792,.T.);
#2617=EDGE_CURVE('',#2090,#2092,#1256,.T.);
#2618=EDGE_CURVE('',#2091,#2092,#1257,.T.);
#2619=EDGE_CURVE('',#2091,#2093,#1793,.T.);
#2620=EDGE_CURVE('',#2092,#2094,#1258,.T.);
#2621=EDGE_CURVE('',#2093,#2094,#1259,.T.);
#2622=EDGE_CURVE('',#2095,#2085,#1794,.T.);
#2623=EDGE_CURVE('',#2095,#2096,#1260,.T.);
#2624=EDGE_CURVE('',#2096,#2087,#1261,.T.);
#2625=EDGE_CURVE('',#2093,#2095,#1795,.T.);
#2626=EDGE_CURVE('',#2094,#2096,#1262,.T.);
#2627=EDGE_CURVE('',#2097,#2098,#1796,.T.);
#2628=EDGE_CURVE('',#2099,#2097,#1797,.T.);
#2629=EDGE_CURVE('',#2099,#2100,#1798,.T.);
#2630=EDGE_CURVE('',#2098,#2099,#1799,.T.);
#2631=EDGE_CURVE('',#2101,#2098,#1800,.T.);
#2632=EDGE_CURVE('',#2102,#2102,#1801,.T.);
#2633=EDGE_CURVE('',#2073,#2102,#1263,.T.);
#2634=EDGE_CURVE('',#2075,#2071,#1802,.T.);
#2635=EDGE_CURVE('',#2082,#2076,#1803,.T.);
#2636=EDGE_CURVE('',#2097,#2084,#1264,.T.);
#3473=ORIENTED_EDGE('',*,*,#2554,.F.);
#3474=ORIENTED_EDGE('',*,*,#2555,.T.);
#3475=ORIENTED_EDGE('',*,*,#2556,.T.);
#3476=ORIENTED_EDGE('',*,*,#2557,.T.);
#3477=ORIENTED_EDGE('',*,*,#2558,.F.);
#3478=ORIENTED_EDGE('',*,*,#2559,.T.);
#3479=ORIENTED_EDGE('',*,*,#2554,.T.);
#3480=ORIENTED_EDGE('',*,*,#2560,.T.);
#3481=ORIENTED_EDGE('',*,*,#2561,.F.);
#3482=ORIENTED_EDGE('',*,*,#2562,.T.);
#3483=ORIENTED_EDGE('',*,*,#2558,.T.);
#3484=ORIENTED_EDGE('',*,*,#2563,.T.);
#3485=ORIENTED_EDGE('',*,*,#2564,.F.);
#3486=ORIENTED_EDGE('',*,*,#2565,.T.);
#3487=ORIENTED_EDGE('',*,*,#2561,.T.);
#3488=ORIENTED_EDGE('',*,*,#2566,.T.);
#3489=ORIENTED_EDGE('',*,*,#2567,.F.);
#3490=ORIENTED_EDGE('',*,*,#2568,.T.);
#3491=ORIENTED_EDGE('',*,*,#2564,.T.);
#3492=ORIENTED_EDGE('',*,*,#2569,.T.);
#3493=ORIENTED_EDGE('',*,*,#2570,.F.);
#3494=ORIENTED_EDGE('',*,*,#2571,.T.);
#3495=ORIENTED_EDGE('',*,*,#2572,.F.);
#3496=ORIENTED_EDGE('',*,*,#2573,.F.);
#3497=ORIENTED_EDGE('',*,*,#2574,.F.);
#3498=ORIENTED_EDGE('',*,*,#2575,.T.);
#3499=ORIENTED_EDGE('',*,*,#2570,.T.);
#3500=ORIENTED_EDGE('',*,*,#2576,.F.);
#3501=ORIENTED_EDGE('',*,*,#2577,.F.);
#3502=ORIENTED_EDGE('',*,*,#2578,.T.);
#3503=ORIENTED_EDGE('',*,*,#2574,.T.);
#3504=ORIENTED_EDGE('',*,*,#2579,.F.);
#3505=ORIENTED_EDGE('',*,*,#2580,.F.);
#3506=ORIENTED_EDGE('',*,*,#2581,.T.);
#3507=ORIENTED_EDGE('',*,*,#2577,.T.);
#3508=ORIENTED_EDGE('',*,*,#2582,.F.);
#3509=ORIENTED_EDGE('',*,*,#2583,.F.);
#3510=ORIENTED_EDGE('',*,*,#2584,.T.);
#3511=ORIENTED_EDGE('',*,*,#2580,.T.);
#3512=ORIENTED_EDGE('',*,*,#2585,.F.);
#3513=ORIENTED_EDGE('',*,*,#2586,.F.);
#3514=ORIENTED_EDGE('',*,*,#2587,.F.);
#3515=ORIENTED_EDGE('',*,*,#2569,.F.);
#3516=ORIENTED_EDGE('',*,*,#2566,.F.);
#3517=ORIENTED_EDGE('',*,*,#2563,.F.);
#3518=ORIENTED_EDGE('',*,*,#2560,.F.);
#3519=ORIENTED_EDGE('',*,*,#2557,.F.);
#3520=ORIENTED_EDGE('',*,*,#2588,.F.);
#3521=ORIENTED_EDGE('',*,*,#2589,.T.);
#3522=ORIENTED_EDGE('',*,*,#2585,.T.);
#3523=ORIENTED_EDGE('',*,*,#2582,.T.);
#3524=ORIENTED_EDGE('',*,*,#2579,.T.);
#3525=ORIENTED_EDGE('',*,*,#2576,.T.);
#3526=ORIENTED_EDGE('',*,*,#2573,.T.);
#3527=ORIENTED_EDGE('',*,*,#2590,.T.);
#3528=ORIENTED_EDGE('',*,*,#2591,.T.);
#3529=ORIENTED_EDGE('',*,*,#2592,.T.);
#3530=ORIENTED_EDGE('',*,*,#2593,.T.);
#3531=ORIENTED_EDGE('',*,*,#2588,.T.);
#3532=ORIENTED_EDGE('',*,*,#2583,.T.);
#3533=ORIENTED_EDGE('',*,*,#2589,.F.);
#3534=ORIENTED_EDGE('',*,*,#2593,.F.);
#3535=ORIENTED_EDGE('',*,*,#2594,.T.);
#3536=ORIENTED_EDGE('',*,*,#2595,.F.);
#3537=ORIENTED_EDGE('',*,*,#2571,.F.);
#3538=ORIENTED_EDGE('',*,*,#2575,.F.);
#3539=ORIENTED_EDGE('',*,*,#2578,.F.);
#3540=ORIENTED_EDGE('',*,*,#2581,.F.);
#3541=ORIENTED_EDGE('',*,*,#2584,.F.);
#3542=ORIENTED_EDGE('',*,*,#2594,.F.);
#3543=ORIENTED_EDGE('',*,*,#2592,.F.);
#3544=ORIENTED_EDGE('',*,*,#2555,.F.);
#3545=ORIENTED_EDGE('',*,*,#2559,.F.);
#3546=ORIENTED_EDGE('',*,*,#2562,.F.);
#3547=ORIENTED_EDGE('',*,*,#2565,.F.);
#3548=ORIENTED_EDGE('',*,*,#2568,.F.);
#3549=ORIENTED_EDGE('',*,*,#2596,.F.);
#3550=ORIENTED_EDGE('',*,*,#2597,.F.);
#3551=ORIENTED_EDGE('',*,*,#2598,.F.);
#3552=ORIENTED_EDGE('',*,*,#2599,.F.);
#3553=ORIENTED_EDGE('',*,*,#2600,.F.);
#3554=ORIENTED_EDGE('',*,*,#2601,.F.);
#3555=ORIENTED_EDGE('',*,*,#2602,.F.);
#3556=ORIENTED_EDGE('',*,*,#2603,.F.);
#3557=ORIENTED_EDGE('',*,*,#2604,.F.);
#3558=ORIENTED_EDGE('',*,*,#2600,.T.);
#3559=ORIENTED_EDGE('',*,*,#2605,.T.);
#3560=ORIENTED_EDGE('',*,*,#2604,.T.);
#3561=ORIENTED_EDGE('',*,*,#2606,.T.);
#3562=ORIENTED_EDGE('',*,*,#2607,.F.);
#3563=ORIENTED_EDGE('',*,*,#2599,.T.);
#3564=ORIENTED_EDGE('',*,*,#2608,.T.);
#3565=ORIENTED_EDGE('',*,*,#2601,.T.);
#3566=ORIENTED_EDGE('',*,*,#2605,.F.);
#3567=ORIENTED_EDGE('',*,*,#2609,.F.);
#3568=ORIENTED_EDGE('',*,*,#2610,.T.);
#3569=ORIENTED_EDGE('',*,*,#2611,.T.);
#3570=ORIENTED_EDGE('',*,*,#2612,.F.);
#3571=ORIENTED_EDGE('',*,*,#2613,.F.);
#3572=ORIENTED_EDGE('',*,*,#2612,.T.);
#3573=ORIENTED_EDGE('',*,*,#2614,.T.);
#3574=ORIENTED_EDGE('',*,*,#2615,.F.);
#3575=ORIENTED_EDGE('',*,*,#2616,.F.);
#3576=ORIENTED_EDGE('',*,*,#2615,.T.);
#3577=ORIENTED_EDGE('',*,*,#2617,.T.);
#3578=ORIENTED_EDGE('',*,*,#2618,.F.);
#3579=ORIENTED_EDGE('',*,*,#2619,.F.);
#3580=ORIENTED_EDGE('',*,*,#2618,.T.);
#3581=ORIENTED_EDGE('',*,*,#2620,.T.);
#3582=ORIENTED_EDGE('',*,*,#2621,.F.);
#3583=ORIENTED_EDGE('',*,*,#2622,.F.);
#3584=ORIENTED_EDGE('',*,*,#2623,.T.);
#3585=ORIENTED_EDGE('',*,*,#2624,.T.);
#3586=ORIENTED_EDGE('',*,*,#2610,.F.);
#3587=ORIENTED_EDGE('',*,*,#2625,.F.);
#3588=ORIENTED_EDGE('',*,*,#2621,.T.);
#3589=ORIENTED_EDGE('',*,*,#2626,.T.);
#3590=ORIENTED_EDGE('',*,*,#2623,.F.);
#3591=ORIENTED_EDGE('',*,*,#2626,.F.);
#3592=ORIENTED_EDGE('',*,*,#2620,.F.);
#3593=ORIENTED_EDGE('',*,*,#2617,.F.);
#3594=ORIENTED_EDGE('',*,*,#2614,.F.);
#3595=ORIENTED_EDGE('',*,*,#2611,.F.);
#3596=ORIENTED_EDGE('',*,*,#2624,.F.);
#3597=ORIENTED_EDGE('',*,*,#2627,.F.);
#3598=ORIENTED_EDGE('',*,*,#2628,.F.);
#3599=ORIENTED_EDGE('',*,*,#2629,.T.);
#3600=ORIENTED_EDGE('',*,*,#2629,.F.);
#3601=ORIENTED_EDGE('',*,*,#2630,.F.);
#3602=ORIENTED_EDGE('',*,*,#2631,.F.);
#3603=ORIENTED_EDGE('',*,*,#2631,.T.);
#3604=ORIENTED_EDGE('',*,*,#2619,.T.);
#3605=ORIENTED_EDGE('',*,*,#2625,.T.);
#3606=ORIENTED_EDGE('',*,*,#2622,.T.);
#3607=ORIENTED_EDGE('',*,*,#2609,.T.);
#3608=ORIENTED_EDGE('',*,*,#2613,.T.);
#3609=ORIENTED_EDGE('',*,*,#2616,.T.);
#3610=ORIENTED_EDGE('',*,*,#2632,.F.);
#3611=ORIENTED_EDGE('',*,*,#2590,.F.);
#3612=ORIENTED_EDGE('',*,*,#2556,.F.);
#3613=ORIENTED_EDGE('',*,*,#2591,.F.);
#3614=ORIENTED_EDGE('',*,*,#2633,.T.);
#3615=ORIENTED_EDGE('',*,*,#2632,.T.);
#3616=ORIENTED_EDGE('',*,*,#2633,.F.);
#3617=ORIENTED_EDGE('',*,*,#2567,.T.);
#3618=ORIENTED_EDGE('',*,*,#2587,.T.);
#3619=ORIENTED_EDGE('',*,*,#2634,.F.);
#3620=ORIENTED_EDGE('',*,*,#2596,.T.);
#3621=ORIENTED_EDGE('',*,*,#2598,.T.);
#3622=ORIENTED_EDGE('',*,*,#2635,.F.);
#3623=ORIENTED_EDGE('',*,*,#2602,.T.);
#3624=ORIENTED_EDGE('',*,*,#2608,.F.);
#3625=ORIENTED_EDGE('',*,*,#2634,.T.);
#3626=ORIENTED_EDGE('',*,*,#2586,.T.);
#3627=ORIENTED_EDGE('',*,*,#2572,.T.);
#3628=ORIENTED_EDGE('',*,*,#2595,.T.);
#3629=ORIENTED_EDGE('',*,*,#2597,.T.);
#3630=ORIENTED_EDGE('',*,*,#2606,.F.);
#3631=ORIENTED_EDGE('',*,*,#2603,.T.);
#3632=ORIENTED_EDGE('',*,*,#2635,.T.);
#3633=ORIENTED_EDGE('',*,*,#2627,.T.);
#3634=ORIENTED_EDGE('',*,*,#2630,.T.);
#3635=ORIENTED_EDGE('',*,*,#2628,.T.);
#3636=ORIENTED_EDGE('',*,*,#2636,.T.);
#3637=ORIENTED_EDGE('',*,*,#2607,.T.);
#3638=ORIENTED_EDGE('',*,*,#2636,.F.);
#4170=CONICAL_SURFACE('',#4890,1.15,0.785398163397449);
#4325=ADVANCED_FACE('',(#658),#469,.T.);
#4326=ADVANCED_FACE('',(#659),#470,.T.);
#4327=ADVANCED_FACE('',(#660),#471,.T.);
#4328=ADVANCED_FACE('',(#661),#472,.T.);
#4329=ADVANCED_FACE('',(#662),#473,.T.);
#4330=ADVANCED_FACE('',(#663),#474,.T.);
#4331=ADVANCED_FACE('',(#664),#475,.T.);
#4332=ADVANCED_FACE('',(#665),#476,.T.);
#4333=ADVANCED_FACE('',(#666),#477,.T.);
#4334=ADVANCED_FACE('',(#667),#478,.T.);
#4335=ADVANCED_FACE('',(#668),#82,.F.);
#4336=ADVANCED_FACE('',(#669),#380,.T.);
#4337=ADVANCED_FACE('',(#670),#479,.T.);
#4338=ADVANCED_FACE('',(#671),#83,.F.);
#4339=ADVANCED_FACE('',(#672),#381,.F.);
#4340=ADVANCED_FACE('',(#673),#382,.F.);
#4341=ADVANCED_FACE('',(#674,#307),#383,.T.);
#4342=ADVANCED_FACE('',(#675),#480,.T.);
#4343=ADVANCED_FACE('',(#676),#384,.F.);
#4344=ADVANCED_FACE('',(#677),#385,.F.);
#4345=ADVANCED_FACE('',(#678),#386,.F.);
#4346=ADVANCED_FACE('',(#679),#387,.F.);
#4347=ADVANCED_FACE('',(#680),#388,.F.);
#4348=ADVANCED_FACE('',(#681),#389,.F.);
#4349=ADVANCED_FACE('',(#682),#390,.F.);
#4350=ADVANCED_FACE('',(#683,#308),#79,.T.);
#4351=ADVANCED_FACE('',(#684),#391,.T.);
#4352=ADVANCED_FACE('',(#685),#4170,.T.);
#4353=ADVANCED_FACE('',(#686),#481,.T.);
#4354=ADVANCED_FACE('',(#687,#309),#392,.T.);
#4355=ADVANCED_FACE('',(#688),#482,.T.);
#4356=ADVANCED_FACE('',(#689),#483,.T.);
#4467=CLOSED_SHELL('',(#4325,#4326,#4327,#4328,#4329,#4330,#4331,#4332,
#4333,#4334,#4335,#4336,#4337,#4338,#4339,#4340,#4341,#4342,#4343,#4344,
#4345,#4346,#4347,#4348,#4349,#4350,#4351,#4352,#4353,#4354,#4355,#4356));
#4843=AXIS2_PLACEMENT_3D('',#8016,#5689,#5690);
#4844=AXIS2_PLACEMENT_3D('',#8017,#5691,#5692);
#4845=AXIS2_PLACEMENT_3D('',#8033,#5694,#5695);
#4846=AXIS2_PLACEMENT_3D('',#8041,#5696,#5697);
#4847=AXIS2_PLACEMENT_3D('',#8089,#5699,#5700);
#4848=AXIS2_PLACEMENT_3D('',#8140,#5702,#5703);
#4849=AXIS2_PLACEMENT_3D('',#8191,#5705,#5706);
#4850=AXIS2_PLACEMENT_3D('',#8239,#5708,#5709);
#4851=AXIS2_PLACEMENT_3D('',#8251,#5711,#5712);
#4852=AXIS2_PLACEMENT_3D('',#8256,#5713,#5714);
#4853=AXIS2_PLACEMENT_3D('',#8281,#5716,#5717);
#4854=AXIS2_PLACEMENT_3D('',#8305,#5719,#5720);
#4855=AXIS2_PLACEMENT_3D('',#8331,#5722,#5723);
#4856=AXIS2_PLACEMENT_3D('',#8688,#5725,#5726);
#4857=AXIS2_PLACEMENT_3D('',#8690,#5727,#5728);
#4858=AXIS2_PLACEMENT_3D('',#8691,#5729,#5730);
#4859=AXIS2_PLACEMENT_3D('',#8775,#5731,#5732);
#4860=AXIS2_PLACEMENT_3D('',#8776,#5733,#5734);
#4861=AXIS2_PLACEMENT_3D('',#9023,#5735,#5736);
#4862=AXIS2_PLACEMENT_3D('',#9032,#5741,#5742);
#4863=AXIS2_PLACEMENT_3D('',#9041,#5747,#5748);
#4864=AXIS2_PLACEMENT_3D('',#9042,#5749,#5750);
#4865=AXIS2_PLACEMENT_3D('',#9043,#5751,#5752);
#4866=AXIS2_PLACEMENT_3D('',#9045,#5753,#5754);
#4867=AXIS2_PLACEMENT_3D('',#9046,#5755,#5756);
#4868=AXIS2_PLACEMENT_3D('',#9047,#5757,#5758);
#4869=AXIS2_PLACEMENT_3D('',#9048,#5759,#5760);
#4870=AXIS2_PLACEMENT_3D('',#9051,#5761,#5762);
#4871=AXIS2_PLACEMENT_3D('',#9057,#5766,#5767);
#4872=AXIS2_PLACEMENT_3D('',#9059,#5768,#5769);
#4873=AXIS2_PLACEMENT_3D('',#9063,#5772,#5773);
#4874=AXIS2_PLACEMENT_3D('',#9065,#5774,#5775);
#4875=AXIS2_PLACEMENT_3D('',#9069,#5778,#5779);
#4876=AXIS2_PLACEMENT_3D('',#9071,#5780,#5781);
#4877=AXIS2_PLACEMENT_3D('',#9075,#5784,#5785);
#4878=AXIS2_PLACEMENT_3D('',#9077,#5786,#5787);
#4879=AXIS2_PLACEMENT_3D('',#9081,#5790,#5791);
#4880=AXIS2_PLACEMENT_3D('',#9082,#5792,#5793);
#4881=AXIS2_PLACEMENT_3D('',#9084,#5795,#5796);
#4882=AXIS2_PLACEMENT_3D('',#9085,#5797,#5798);
#4883=AXIS2_PLACEMENT_3D('',#9088,#5799,#5800);
#4884=AXIS2_PLACEMENT_3D('',#9090,#5801,#5802);
#4885=AXIS2_PLACEMENT_3D('',#9092,#5803,#5804);
#4886=AXIS2_PLACEMENT_3D('',#9093,#5805,#5806);
#4887=AXIS2_PLACEMENT_3D('',#9095,#5807,#5808);
#4888=AXIS2_PLACEMENT_3D('',#9096,#5809,#5810);
#4889=AXIS2_PLACEMENT_3D('',#9098,#5811,#5812);
#4890=AXIS2_PLACEMENT_3D('',#9099,#5813,#5814);
#4891=AXIS2_PLACEMENT_3D('',#9101,#5816,#5817);
#4892=AXIS2_PLACEMENT_3D('',#9102,#5818,#5819);
#4893=AXIS2_PLACEMENT_3D('',#9103,#5820,#5821);
#4894=AXIS2_PLACEMENT_3D('',#9104,#5822,#5823);
#4895=AXIS2_PLACEMENT_3D('',#9105,#5824,#5825);
#4896=AXIS2_PLACEMENT_3D('',#9106,#5826,#5827);
#5689=DIRECTION('axis',(0.,0.,1.));
#5690=DIRECTION('refdir',(1.,0.,0.));
#5691=DIRECTION('center_axis',(1.,0.,0.));
#5692=DIRECTION('ref_axis',(0.,1.,0.));
#5693=DIRECTION('',(-1.,0.,0.));
#5694=DIRECTION('center_axis',(1.,0.,0.));
#5695=DIRECTION('ref_axis',(0.,1.,0.));
#5696=DIRECTION('center_axis',(1.,0.,0.));
#5697=DIRECTION('ref_axis',(0.,1.,0.));
#5698=DIRECTION('',(-1.,0.,0.));
#5699=DIRECTION('center_axis',(1.,0.,0.));
#5700=DIRECTION('ref_axis',(0.,1.,0.));
#5701=DIRECTION('',(-1.,0.,0.));
#5702=DIRECTION('center_axis',(1.,0.,0.));
#5703=DIRECTION('ref_axis',(0.,1.,0.));
#5704=DIRECTION('',(-1.,0.,0.));
#5705=DIRECTION('center_axis',(1.,0.,0.));
#5706=DIRECTION('ref_axis',(0.,1.,0.));
#5707=DIRECTION('',(-1.,0.,0.));
#5708=DIRECTION('center_axis',(1.,0.,0.));
#5709=DIRECTION('ref_axis',(0.,-0.548549944708551,-0.836117789644644));
#5710=DIRECTION('',(1.,0.,0.));
#5711=DIRECTION('center_axis',(1.,0.,0.));
#5712=DIRECTION('ref_axis',(0.,1.,2.56286223017387E-15));
#5713=DIRECTION('center_axis',(1.,0.,0.));
#5714=DIRECTION('ref_axis',(0.,1.,2.56286223017387E-15));
#5715=DIRECTION('',(1.,0.,0.));
#5716=DIRECTION('center_axis',(1.,0.,0.));
#5717=DIRECTION('ref_axis',(0.,1.,2.56286223017387E-15));
#5718=DIRECTION('',(1.,0.,0.));
#5719=DIRECTION('center_axis',(1.,0.,0.));
#5720=DIRECTION('ref_axis',(0.,1.,2.56286223017387E-15));
#5721=DIRECTION('',(1.,0.,0.));
#5722=DIRECTION('center_axis',(1.,0.,0.));
#5723=DIRECTION('ref_axis',(0.,1.,2.56286223017387E-15));
#5724=DIRECTION('',(1.,0.,0.));
#5725=DIRECTION('center_axis',(1.,0.,0.));
#5726=DIRECTION('ref_axis',(0.,0.,-1.));
#5727=DIRECTION('center_axis',(1.,0.,0.));
#5728=DIRECTION('ref_axis',(0.,1.,0.));
#5729=DIRECTION('center_axis',(1.,0.,0.));
#5730=DIRECTION('ref_axis',(0.,1.,0.));
#5731=DIRECTION('center_axis',(-1.,0.,0.));
#5732=DIRECTION('ref_axis',(0.,1.,2.56286223017387E-15));
#5733=DIRECTION('center_axis',(1.,0.,0.));
#5734=DIRECTION('ref_axis',(0.,0.889057334805044,0.457795866549002));
#5735=DIRECTION('center_axis',(0.,-1.,0.));
#5736=DIRECTION('ref_axis',(0.,0.,-1.));
#5737=DIRECTION('',(1.,0.,0.));
#5738=DIRECTION('',(0.,0.,-1.));
#5739=DIRECTION('',(-1.,0.,0.));
#5740=DIRECTION('',(0.,0.,1.));
#5741=DIRECTION('center_axis',(0.,1.,0.));
#5742=DIRECTION('ref_axis',(0.,0.,1.));
#5743=DIRECTION('',(1.,0.,0.));
#5744=DIRECTION('',(0.,0.,1.));
#5745=DIRECTION('',(-1.,0.,0.));
#5746=DIRECTION('',(0.,0.,-1.));
#5747=DIRECTION('center_axis',(1.,0.,0.));
#5748=DIRECTION('ref_axis',(0.,0.,-1.));
#5749=DIRECTION('center_axis',(1.,0.,0.));
#5750=DIRECTION('ref_axis',(0.,0.,-1.));
#5751=DIRECTION('center_axis',(1.,0.,0.));
#5752=DIRECTION('ref_axis',(0.,0.,-1.));
#5753=DIRECTION('center_axis',(1.,0.,0.));
#5754=DIRECTION('ref_axis',(0.,0.,-1.));
#5755=DIRECTION('center_axis',(1.,0.,0.));
#5756=DIRECTION('ref_axis',(0.,1.,0.));
#5757=DIRECTION('center_axis',(1.,0.,0.));
#5758=DIRECTION('ref_axis',(0.,0.,-1.));
#5759=DIRECTION('center_axis',(0.,-0.5,-0.866025403784439));
#5760=DIRECTION('ref_axis',(0.,-0.866025403784439,0.5));
#5761=DIRECTION('center_axis',(0.,-0.5,-0.866025403784439));
#5762=DIRECTION('ref_axis',(0.,-0.866025403784439,0.5));
#5763=DIRECTION('',(-1.,0.,0.));
#5764=DIRECTION('',(0.,-0.866025403784439,0.5));
#5765=DIRECTION('',(-1.,0.,0.));
#5766=DIRECTION('center_axis',(0.,-1.,-1.60246890531964E-16));
#5767=DIRECTION('ref_axis',(0.,-1.60246890531964E-16,1.));
#5768=DIRECTION('center_axis',(0.,-1.,-1.60246890531964E-16));
#5769=DIRECTION('ref_axis',(0.,-1.60246890531964E-16,1.));
#5770=DIRECTION('',(0.,-1.60246890531964E-16,1.));
#5771=DIRECTION('',(-1.,0.,0.));
#5772=DIRECTION('center_axis',(0.,-0.5,0.866025403784439));
#5773=DIRECTION('ref_axis',(0.,0.866025403784439,0.5));
#5774=DIRECTION('center_axis',(0.,-0.5,0.866025403784439));
#5775=DIRECTION('ref_axis',(0.,0.866025403784439,0.5));
#5776=DIRECTION('',(0.,0.866025403784439,0.5));
#5777=DIRECTION('',(-1.,0.,0.));
#5778=DIRECTION('center_axis',(0.,0.5,0.866025403784439));
#5779=DIRECTION('ref_axis',(0.,0.866025403784439,-0.5));
#5780=DIRECTION('center_axis',(0.,0.5,0.866025403784439));
#5781=DIRECTION('ref_axis',(0.,0.866025403784439,-0.5));
#5782=DIRECTION('',(0.,0.866025403784439,-0.5));
#5783=DIRECTION('',(-1.,0.,0.));
#5784=DIRECTION('center_axis',(0.,0.5,-0.866025403784439));
#5785=DIRECTION('ref_axis',(0.,-0.866025403784439,-0.5));
#5786=DIRECTION('center_axis',(0.,0.5,-0.866025403784439));
#5787=DIRECTION('ref_axis',(0.,-0.866025403784439,-0.5));
#5788=DIRECTION('',(-1.,0.,0.));
#5789=DIRECTION('',(0.,-0.866025403784439,-0.5));
#5790=DIRECTION('center_axis',(0.,1.,-3.20493781063927E-16));
#5791=DIRECTION('ref_axis',(0.,-3.20493781063927E-16,-1.));
#5792=DIRECTION('center_axis',(0.,1.,-3.20493781063927E-16));
#5793=DIRECTION('ref_axis',(0.,-3.20493781063927E-16,-1.));
#5794=DIRECTION('',(0.,-3.20493781063927E-16,-1.));
#5795=DIRECTION('center_axis',(-1.,0.,0.));
#5796=DIRECTION('ref_axis',(0.,0.,1.));
#5797=DIRECTION('center_axis',(0.,0.,1.));
#5798=DIRECTION('ref_axis',(1.,0.,0.));
#5799=DIRECTION('center_axis',(-1.,0.,0.));
#5800=DIRECTION('ref_axis',(0.,1.,0.));
#5801=DIRECTION('center_axis',(-1.,0.,0.));
#5802=DIRECTION('ref_axis',(0.,1.,0.));
#5803=DIRECTION('center_axis',(1.22464679914735E-16,-1.,0.));
#5804=DIRECTION('ref_axis',(-1.,-1.22464679914735E-16,0.));
#5805=DIRECTION('center_axis',(-1.,0.,0.));
#5806=DIRECTION('ref_axis',(0.,1.,0.));
#5807=DIRECTION('center_axis',(1.22464679914735E-16,-1.,0.));
#5808=DIRECTION('ref_axis',(-1.,-1.22464679914735E-16,0.));
#5809=DIRECTION('center_axis',(-1.,0.,0.));
#5810=DIRECTION('ref_axis',(0.,0.,1.));
#5811=DIRECTION('center_axis',(1.,0.,0.));
#5812=DIRECTION('ref_axis',(0.,0.,-1.));
#5813=DIRECTION('center_axis',(1.,0.,0.));
#5814=DIRECTION('ref_axis',(0.,1.,0.));
#5815=DIRECTION('',(-0.707106781186547,0.707106781186548,8.65956056235494E-17));
#5816=DIRECTION('center_axis',(1.,0.,0.));
#5817=DIRECTION('ref_axis',(0.,1.,0.));
#5818=DIRECTION('center_axis',(1.,0.,0.));
#5819=DIRECTION('ref_axis',(0.,1.,0.));
#5820=DIRECTION('center_axis',(-1.,0.,0.));
#5821=DIRECTION('ref_axis',(0.,0.,1.));
#5822=DIRECTION('center_axis',(1.,0.,0.));
#5823=DIRECTION('ref_axis',(0.,0.,-1.));
#5824=DIRECTION('center_axis',(1.,0.,0.));
#5825=DIRECTION('ref_axis',(0.,1.,0.));
#5826=DIRECTION('center_axis',(1.,0.,0.));
#5827=DIRECTION('ref_axis',(0.,1.,0.));
#5828=DIRECTION('',(-1.,0.,0.));
#8016=CARTESIAN_POINT('',(0.,0.,0.));
#8017=CARTESIAN_POINT('Origin',(-1.1,0.,0.));
#8018=CARTESIAN_POINT('',(-2.09010734985006,-1.21555704018822,0.00101556544434535));
#8019=CARTESIAN_POINT('',(-2.15489265014994,-1.21581627598942,0.00130132384810224));
#8020=CARTESIAN_POINT('',(-1.1,-1.215,-1.48794586096403E-16));
#8021=CARTESIAN_POINT('',(-2.235,0.531593232241059,1.09337941589937));
#8022=CARTESIAN_POINT('Ctrl Pts',(-2.09010734985006,-1.21555704018822,0.00101556544434535));
#8023=CARTESIAN_POINT('Ctrl Pts',(-2.09435627684546,-1.21616855233654,0.0729895168668011));
#8024=CARTESIAN_POINT('Ctrl Pts',(-2.09860520384087,-1.2103032966511,0.144859657339869));
#8025=CARTESIAN_POINT('Ctrl Pts',(-2.10285413083627,-1.19759745787725,0.215493040591908));
#8026=CARTESIAN_POINT('Ctrl Pts',(-2.12621917673445,-1.1277274633005,0.603909279188963));
#8027=CARTESIAN_POINT('Ctrl Pts',(-2.14958422263263,-0.85100159321999,0.954926586373963));
#8028=CARTESIAN_POINT('Ctrl Pts',(-2.17294926853081,-0.489637107432698,
1.11385746442067));
#8029=CARTESIAN_POINT('Ctrl Pts',(-2.19363284568721,-0.169744295925529,
1.25454878139639));
#8030=CARTESIAN_POINT('Ctrl Pts',(-2.2143164228436,0.216474938558358,1.24471299392075));
#8031=CARTESIAN_POINT('Ctrl Pts',(-2.235,0.532202955181985,1.09392695412892));
#8032=CARTESIAN_POINT('',(-2.235,-0.530983509300121,1.09283187766981));
#8033=CARTESIAN_POINT('Origin',(-2.235,0.,0.));
#8034=CARTESIAN_POINT('Ctrl Pts',(-2.235,-0.53098350930012,1.09283187766981));
#8035=CARTESIAN_POINT('Ctrl Pts',(-2.21163495410182,-0.887506341491207,
0.919605100110861));
#8036=CARTESIAN_POINT('Ctrl Pts',(-2.18826990820364,-1.15001549756272,0.560130039467285));
#8037=CARTESIAN_POINT('Ctrl Pts',(-2.16490486230546,-1.20483997833738,0.169869648085053));
#8038=CARTESIAN_POINT('Ctrl Pts',(-2.16156745825362,-1.21267096848714,0.114125840983309));
#8039=CARTESIAN_POINT('Ctrl Pts',(-2.15823005420178,-1.21626466312913,0.0577539348489441));
#8040=CARTESIAN_POINT('Ctrl Pts',(-2.15489265014994,-1.21581627598942,0.00130132384810224));
#8041=CARTESIAN_POINT('Origin',(-1.1,0.,0.));
#8042=CARTESIAN_POINT('',(-1.64010734985006,-1.21347552231432,-0.000575546447129233));
#8043=CARTESIAN_POINT('',(-1.70489265014994,-1.21328542726779,-0.000363737954992407));
#8044=CARTESIAN_POINT('',(-1.1,-1.215,-1.48794586096403E-16));
#8045=CARTESIAN_POINT('Ctrl Pts',(-1.64010734985006,-1.21347552231432,-0.000575546447129233));
#8046=CARTESIAN_POINT('Ctrl Pts',(-1.65416600145638,-1.21240787552406,0.238620955458428));
#8047=CARTESIAN_POINT('Ctrl Pts',(-1.6682246530627,-1.14377867336048,0.478382638558954));
#8048=CARTESIAN_POINT('Ctrl Pts',(-1.68228330466901,-1.01186572903878,0.675872676498389));
#8049=CARTESIAN_POINT('Ctrl Pts',(-1.7056483505672,-0.792630479105178,1.00409503594676));
#8050=CARTESIAN_POINT('Ctrl Pts',(-1.72901339646538,-0.398596571949964,
1.21555712552604));
#8051=CARTESIAN_POINT('Ctrl Pts',(-1.75237844236356,-0.00388959740550279,
1.21682095992699));
#8052=CARTESIAN_POINT('Ctrl Pts',(-1.77574348826174,0.39081737713896,1.21808479432795));
#8053=CARTESIAN_POINT('Ctrl Pts',(-1.79910853415992,0.78619741907267,1.00915037355058));
#8054=CARTESIAN_POINT('Ctrl Pts',(-1.8224735800581,1.00752575948006,0.682330574304518));
#8055=CARTESIAN_POINT('Ctrl Pts',(-1.84583862595628,1.22885409988745,0.355510775058457));
#8056=CARTESIAN_POINT('Ctrl Pts',(-1.86920367185446,1.27613073876853,-0.0891944026562985));
#8057=CARTESIAN_POINT('Ctrl Pts',(-1.89256871775264,1.12846908484488,-0.455233278205789));
#8058=CARTESIAN_POINT('Ctrl Pts',(-1.91593376365082,0.980807430921236,-0.821272153755278));
#8059=CARTESIAN_POINT('Ctrl Pts',(-1.939298809549,0.638207484192875,-1.1086447271395));
#8060=CARTESIAN_POINT('Ctrl Pts',(-1.96266385544718,0.252056972817938,-1.19042038674822));
#8061=CARTESIAN_POINT('Ctrl Pts',(-1.98602890134536,-0.134093538557,-1.27219604635694));
#8062=CARTESIAN_POINT('Ctrl Pts',(-2.00939394724354,-0.563794614578515,
-1.14837479219015));
#8063=CARTESIAN_POINT('Ctrl Pts',(-2.03275899314173,-0.847138093052768,
-0.873556580102204));
#8064=CARTESIAN_POINT('Ctrl Pts',(-2.0518751120445,-1.07895564001776,-0.648713982239761));
#8065=CARTESIAN_POINT('Ctrl Pts',(-2.07099123094728,-1.21280581877384,-0.322798568049416));
#8066=CARTESIAN_POINT('Ctrl Pts',(-2.09010734985006,-1.21555704018822,0.00101556544434535));
#8067=CARTESIAN_POINT('Ctrl Pts',(-2.15489265014994,-1.21581627598942,0.00130132384810224));
#8068=CARTESIAN_POINT('Ctrl Pts',(-2.1348650083036,-1.21312552086863,-0.337468767172928));
#8069=CARTESIAN_POINT('Ctrl Pts',(-2.11483736645726,-1.06487305501001,-0.679145167136663));
#8070=CARTESIAN_POINT('Ctrl Pts',(-2.09480972461092,-0.81324537235474,-0.90543373177546));
#8071=CARTESIAN_POINT('Ctrl Pts',(-2.07144467871274,-0.519686480119644,
-1.16943099813285));
#8072=CARTESIAN_POINT('Ctrl Pts',(-2.04807963281455,-0.0854288901716521,
-1.27637980872674));
#8073=CARTESIAN_POINT('Ctrl Pts',(-2.02471458691637,0.297352750944294,-1.17983198073104));
#8074=CARTESIAN_POINT('Ctrl Pts',(-2.00134954101819,0.68013439206024,-1.08328415273534));
#8075=CARTESIAN_POINT('Ctrl Pts',(-1.97798449512001,1.01144008434414,-0.783239686150053));
#8076=CARTESIAN_POINT('Ctrl Pts',(-1.95461944922183,1.14500372357387,-0.411877774273037));
#8077=CARTESIAN_POINT('Ctrl Pts',(-1.93125440332365,1.27856736280359,-0.0405158623960201));
#8078=CARTESIAN_POINT('Ctrl Pts',(-1.90788935742547,1.21438894897914,0.402163494772724));
#8079=CARTESIAN_POINT('Ctrl Pts',(-1.88452431152729,0.98075572302807,0.720320851177092));
#8080=CARTESIAN_POINT('Ctrl Pts',(-1.86115926562911,0.747122497076996,1.03847820758146));
#8081=CARTESIAN_POINT('Ctrl Pts',(-1.83779421973093,0.344034458999299,1.23211356322145));
#8082=CARTESIAN_POINT('Ctrl Pts',(-1.81442917383275,-0.050341458175738,
1.21577086315243));
#8083=CARTESIAN_POINT('Ctrl Pts',(-1.79106412793457,-0.444717375350775,
1.19942816308341));
#8084=CARTESIAN_POINT('Ctrl Pts',(-1.76769908203638,-0.83038117162315,0.973107407305383));
#8085=CARTESIAN_POINT('Ctrl Pts',(-1.7443340361382,-1.03692497416749,0.63676228257843));
#8086=CARTESIAN_POINT('Ctrl Pts',(-1.73118690747545,-1.15314378916056,0.447506389431653));
#8087=CARTESIAN_POINT('Ctrl Pts',(-1.71803977881269,-1.21265091085685,0.223415366285508));
#8088=CARTESIAN_POINT('Ctrl Pts',(-1.70489265014994,-1.21328542726779,-0.000363737954992407));
#8089=CARTESIAN_POINT('Origin',(-1.1,0.,0.));
#8090=CARTESIAN_POINT('',(-1.19010734985006,-1.21680543282056,0.000145867497023454));
#8091=CARTESIAN_POINT('',(-1.25489265014994,-1.21681358531413,-0.000118566432341596));
#8092=CARTESIAN_POINT('',(-1.1,-1.215,-1.48794586096403E-16));
#8093=CARTESIAN_POINT('Ctrl Pts',(-1.19010734985006,-1.21680543282056,0.000145867497023454));
#8094=CARTESIAN_POINT('Ctrl Pts',(-1.19061068016911,-1.21682033874597,0.00864914984812415));
#8095=CARTESIAN_POINT('Ctrl Pts',(-1.19111401048817,-1.21673860976105,0.0171521385756626));
#8096=CARTESIAN_POINT('Ctrl Pts',(-1.19161734080722,-1.21655935421094,0.0256530708019106));
#8097=CARTESIAN_POINT('Ctrl Pts',(-1.2149823867054,-1.20823815042624,0.42027398697765));
#8098=CARTESIAN_POINT('Ctrl Pts',(-1.23834743260358,-0.989756964692678,
0.810463348804642));
#8099=CARTESIAN_POINT('Ctrl Pts',(-1.26171247850176,-0.657664591757992,
1.02379297304796));
#8100=CARTESIAN_POINT('Ctrl Pts',(-1.28507752439994,-0.325572218823306,
1.23712259729128));
#8101=CARTESIAN_POINT('Ctrl Pts',(-1.30844257029812,0.120131341312504,1.27359248395092));
#8102=CARTESIAN_POINT('Ctrl Pts',(-1.3318076161963,0.48248577096526,1.11708642885146));
#8103=CARTESIAN_POINT('Ctrl Pts',(-1.35517266209448,0.844840200618017,0.960580373751996));
#8104=CARTESIAN_POINT('Ctrl Pts',(-1.37853770799267,1.12384549978772,0.611098376893435));
#8105=CARTESIAN_POINT('Ctrl Pts',(-1.40190275389085,1.19620669325149,0.223079283185934));
#8106=CARTESIAN_POINT('Ctrl Pts',(-1.42526779978903,1.26856788671526,-0.164939810521567));
#8107=CARTESIAN_POINT('Ctrl Pts',(-1.44863284568721,1.13428497447309,-0.591496001078011));
#8108=CARTESIAN_POINT('Ctrl Pts',(-1.47199789158539,0.852698879583878,-0.868089649892069));
#8109=CARTESIAN_POINT('Ctrl Pts',(-1.49536293748357,0.571112784694665,-1.14468329870613));
#8110=CARTESIAN_POINT('Ctrl Pts',(-1.51872798338175,0.142223507158407,-1.2713144057778));
#8111=CARTESIAN_POINT('Ctrl Pts',(-1.54209302927993,-0.244439197279475,
-1.19202486410288));
#8112=CARTESIAN_POINT('Ctrl Pts',(-1.56545807517811,-0.631101901717355,
-1.11273532242796));
#8113=CARTESIAN_POINT('Ctrl Pts',(-1.58882312107629,-0.975538033056859,
-0.827525132006445));
#8114=CARTESIAN_POINT('Ctrl Pts',(-1.61218816697447,-1.12553780237062,-0.462428722136953));
#8115=CARTESIAN_POINT('Ctrl Pts',(-1.62149456126633,-1.18528333007065,-0.317009314034972));
#8116=CARTESIAN_POINT('Ctrl Pts',(-1.6308009555582,-1.21418227160102,-0.158916262349573));
#8117=CARTESIAN_POINT('Ctrl Pts',(-1.64010734985006,-1.21347552231432,-0.000575546447129233));
#8118=CARTESIAN_POINT('Ctrl Pts',(-1.70489265014994,-1.21328542726779,-0.000363737954992407));
#8119=CARTESIAN_POINT('Ctrl Pts',(-1.69467473291451,-1.21377857191844,-0.174284327370441));
#8120=CARTESIAN_POINT('Ctrl Pts',(-1.68445681567909,-1.17871053439215,-0.348016506489212));
#8121=CARTESIAN_POINT('Ctrl Pts',(-1.67423889844366,-1.10706686273875,-0.505060300998285));
#8122=CARTESIAN_POINT('Ctrl Pts',(-1.65087385254548,-0.943241139949365,
-0.864168266172182));
#8123=CARTESIAN_POINT('Ctrl Pts',(-1.6275088066473,-0.588165885554272,-1.1360147028441));
#8124=CARTESIAN_POINT('Ctrl Pts',(-1.60414376074912,-0.198757634157503,
-1.20048470038601));
#8125=CARTESIAN_POINT('Ctrl Pts',(-1.58077871485094,0.190650617239263,-1.26495469792792));
#8126=CARTESIAN_POINT('Ctrl Pts',(-1.55741366895276,0.614391865637705,-1.12204825633983));
#8127=CARTESIAN_POINT('Ctrl Pts',(-1.53404862305458,0.885214061026173,-0.834908355079327));
#8128=CARTESIAN_POINT('Ctrl Pts',(-1.5106835771564,1.15603625641464,-0.547768453818826));
#8129=CARTESIAN_POINT('Ctrl Pts',(-1.48731853125821,1.27393939879314,-0.11639509288592));
#8130=CARTESIAN_POINT('Ctrl Pts',(-1.46395348536003,1.18681948727553,0.268579473257125));
#8131=CARTESIAN_POINT('Ctrl Pts',(-1.44058843946185,1.09969957575793,0.653554039400168));
#8132=CARTESIAN_POINT('Ctrl Pts',(-1.41722339356367,0.807556610344237,0.992129810753349));
#8133=CARTESIAN_POINT('Ctrl Pts',(-1.39385834766549,0.439491974942901,1.13468954182857));
#8134=CARTESIAN_POINT('Ctrl Pts',(-1.37049330176731,0.0714273395415663,
1.27724927290379));
#8135=CARTESIAN_POINT('Ctrl Pts',(-1.34712825586913,-0.372558965847411,
1.22379296370105));
#8136=CARTESIAN_POINT('Ctrl Pts',(-1.32376320997095,-0.696265889399082,
0.997942178270234));
#8137=CARTESIAN_POINT('Ctrl Pts',(-1.30080635669728,-1.01431757994704,0.776037057027471));
#8138=CARTESIAN_POINT('Ctrl Pts',(-1.27784950342361,-1.21625579422078,0.387708384054187));
#8139=CARTESIAN_POINT('Ctrl Pts',(-1.25489265014994,-1.21681358531413,-0.000118566432341596));
#8140=CARTESIAN_POINT('Origin',(-1.1,0.,0.));
#8141=CARTESIAN_POINT('',(-0.74010734985006,-1.21327246620193,0.000345136923926501));
#8142=CARTESIAN_POINT('',(-0.804892650149939,-1.21345200008106,0.000555700457907037));
#8143=CARTESIAN_POINT('',(-1.1,-1.215,-1.48794586096403E-16));
#8144=CARTESIAN_POINT('Ctrl Pts',(-0.74010734985006,-1.21327246620193,0.000345136923926501));
#8145=CARTESIAN_POINT('Ctrl Pts',(-0.750420404780028,-1.21373773246957,
0.175887272582135));
#8146=CARTESIAN_POINT('Ctrl Pts',(-0.760733459709996,-1.17798633483971,
0.351249023172776));
#8147=CARTESIAN_POINT('Ctrl Pts',(-0.771046514639964,-1.10504391190561,
0.509464052100677));
#8148=CARTESIAN_POINT('Ctrl Pts',(-0.794411560538145,-0.939787053355631,
0.867912779251391));
#8149=CARTESIAN_POINT('Ctrl Pts',(-0.817776606436326,-0.583634221976302,
1.13834994754172));
#8150=CARTESIAN_POINT('Ctrl Pts',(-0.841141652334506,-0.193972815310299,
1.20126947215299));
#8151=CARTESIAN_POINT('Ctrl Pts',(-0.864506698232687,0.195688591355703,
1.26418899676426));
#8152=CARTESIAN_POINT('Ctrl Pts',(-0.887871744130868,0.618858573308381,
1.11959087769647));
#8153=CARTESIAN_POINT('Ctrl Pts',(-0.911236790029049,0.888534727151963,
0.831372995795705));
#8154=CARTESIAN_POINT('Ctrl Pts',(-0.93460183592723,1.15821088099554,0.54315511389494));
#8155=CARTESIAN_POINT('Ctrl Pts',(-0.957966881825411,1.27439320673003,0.111317469161196));
#8156=CARTESIAN_POINT('Ctrl Pts',(-0.981331927723592,1.18573961955721,-0.273306374200708));
#8157=CARTESIAN_POINT('Ctrl Pts',(-1.00469697362177,1.09708603238439,-0.657930217562613));
#8158=CARTESIAN_POINT('Ctrl Pts',(-1.02806201951995,0.803596532304258,-0.995340259552676));
#8159=CARTESIAN_POINT('Ctrl Pts',(-1.05142706541813,0.434966776615619,-1.13643236136105));
#8160=CARTESIAN_POINT('Ctrl Pts',(-1.07479211131631,0.0663370209269809,
-1.27752446316943));
#8161=CARTESIAN_POINT('Ctrl Pts',(-1.0981571572145,-0.377432990370165,-1.22229862479612));
#8162=CARTESIAN_POINT('Ctrl Pts',(-1.12152220311268,-0.70023738510082,-0.995159470347216));
#8163=CARTESIAN_POINT('Ctrl Pts',(-1.1443839186918,-1.016087920648,-0.772913352427169));
#8164=CARTESIAN_POINT('Ctrl Pts',(-1.16724563427093,-1.21612839228815,-0.386080861236012));
#8165=CARTESIAN_POINT('Ctrl Pts',(-1.19010734985006,-1.21680543282056,0.000145867497023454));
#8166=CARTESIAN_POINT('Ctrl Pts',(-1.25489265014994,-1.21681358531413,-0.000118566432341596));
#8167=CARTESIAN_POINT('Ctrl Pts',(-1.25448445752543,-1.2168235033202,-0.00701446365691278));
#8168=CARTESIAN_POINT('Ctrl Pts',(-1.25407626490092,-1.21676975308714,-0.0139102022573895));
#8169=CARTESIAN_POINT('Ctrl Pts',(-1.25366807227641,-1.21665185527998,-0.0208048438500122));
#8170=CARTESIAN_POINT('Ctrl Pts',(-1.23030302637823,-1.20990335589485,-0.415455818880555));
#8171=CARTESIAN_POINT('Ctrl Pts',(-1.20693798048005,-0.992978815410212,
-0.806512507282753));
#8172=CARTESIAN_POINT('Ctrl Pts',(-1.18357293458187,-0.661739228727891,
-1.02116382620166));
#8173=CARTESIAN_POINT('Ctrl Pts',(-1.16020788868369,-0.330499642045568,
-1.23581514512057));
#8174=CARTESIAN_POINT('Ctrl Pts',(-1.13684284278551,0.11505499083444,-1.27406109455618));
#8175=CARTESIAN_POINT('Ctrl Pts',(-1.11347779688732,0.47803019109439,-1.11900029591178));
#8176=CARTESIAN_POINT('Ctrl Pts',(-1.09011275098914,0.841005391354337,-0.963939497267381));
#8177=CARTESIAN_POINT('Ctrl Pts',(-1.06674770509096,1.12140115899423,-0.615571950542975));
#8178=CARTESIAN_POINT('Ctrl Pts',(-1.04338265919278,1.19530808939557,-0.227844404091649));
#8179=CARTESIAN_POINT('Ctrl Pts',(-1.0200176132946,1.26921501979691,0.159883142359683));
#8180=CARTESIAN_POINT('Ctrl Pts',(-0.996652567396421,1.1366331129597,0.586970688537935));
#8181=CARTESIAN_POINT('Ctrl Pts',(-0.97328752149824,0.856151500849342,0.864684412627987));
#8182=CARTESIAN_POINT('Ctrl Pts',(-0.949922475600059,0.575669888738987,
1.14239813671804));
#8183=CARTESIAN_POINT('Ctrl Pts',(-0.926557429701878,0.147288571355488,
1.27073803871989));
#8184=CARTESIAN_POINT('Ctrl Pts',(-0.903192383803698,-0.239686951572779,
1.19298974514702));
#8185=CARTESIAN_POINT('Ctrl Pts',(-0.879827337905517,-0.626662474501049,
1.11524145157414));
#8186=CARTESIAN_POINT('Ctrl Pts',(-0.856462292007336,-0.972232202974088,
0.831404962426542));
#8187=CARTESIAN_POINT('Ctrl Pts',(-0.833097246109155,-1.12368582435133,
0.466909784257848));
#8188=CARTESIAN_POINT('Ctrl Pts',(-0.82369571412275,-1.18462711554503,0.320245699309042));
#8189=CARTESIAN_POINT('Ctrl Pts',(-0.814294182136344,-1.21413976936114,
0.160522457515797));
#8190=CARTESIAN_POINT('Ctrl Pts',(-0.804892650149939,-1.21345200008106,
0.000555700457907037));
#8191=CARTESIAN_POINT('Origin',(-1.1,0.,0.));
#8192=CARTESIAN_POINT('',(-0.29010734985006,-1.21601418463372,-0.00087989446188777));
#8193=CARTESIAN_POINT('',(-0.354892650149939,-1.2156153315498,-0.000937869499410686));
#8194=CARTESIAN_POINT('',(-1.1,-1.215,-1.48794586096403E-16));
#8195=CARTESIAN_POINT('Ctrl Pts',(-0.29010734985006,-1.21601418463372,-0.00087989446188777));
#8196=CARTESIAN_POINT('Ctrl Pts',(-0.310230129390944,-1.21339239274019,
0.339644417133859));
#8197=CARTESIAN_POINT('Ctrl Pts',(-0.330352908931827,-1.06334626260878,
0.682304929774367));
#8198=CARTESIAN_POINT('Ctrl Pts',(-0.350475688472711,-0.809560818622168,
0.90849068695983));
#8199=CARTESIAN_POINT('Ctrl Pts',(-0.373840734370892,-0.514884403021141,
1.17112043884951));
#8200=CARTESIAN_POINT('Ctrl Pts',(-0.397205780269073,-0.0803456732840405,
1.27671783501035));
#8201=CARTESIAN_POINT('Ctrl Pts',(-0.420570826167254,0.302014387470901,
1.1787369191183));
#8202=CARTESIAN_POINT('Ctrl Pts',(-0.443935872065435,0.684374448225843,
1.08075600322626));
#8203=CARTESIAN_POINT('Ctrl Pts',(-0.467300917963614,1.01455583999862,0.779196775281337));
#8204=CARTESIAN_POINT('Ctrl Pts',(-0.490665963861795,1.14665608671571,0.407258679262273));
#8205=CARTESIAN_POINT('Ctrl Pts',(-0.514031009759976,1.27875633343279,0.0353205832432076));
#8206=CARTESIAN_POINT('Ctrl Pts',(-0.537396055658157,1.21277543509418,-0.406996380850001));
#8207=CARTESIAN_POINT('Ctrl Pts',(-0.560761101556338,0.977866936696777,
-0.724195707500305));
#8208=CARTESIAN_POINT('Ctrl Pts',(-0.584126147454519,0.74295843829938,-1.04139503415061));
#8209=CARTESIAN_POINT('Ctrl Pts',(-0.6074911933527,0.339122339843202,-1.23347672335801));
#8210=CARTESIAN_POINT('Ctrl Pts',(-0.63085623925088,-0.0551805065988665,
-1.21557537371284));
#8211=CARTESIAN_POINT('Ctrl Pts',(-0.654221285149061,-0.449483353040935,
-1.19767402406768));
#8212=CARTESIAN_POINT('Ctrl Pts',(-0.677586331047242,-0.834252947468894,
-0.969789635569952));
#8213=CARTESIAN_POINT('Ctrl Pts',(-0.700951376945423,-1.03945730182256,
-0.632617298315537));
#8214=CARTESIAN_POINT('Ctrl Pts',(-0.714003367913635,-1.15408688103817,
-0.444268843116553));
#8215=CARTESIAN_POINT('Ctrl Pts',(-0.727055358881848,-1.21268363474857,
-0.221817392482749));
#8216=CARTESIAN_POINT('Ctrl Pts',(-0.74010734985006,-1.21327246620193,0.000345136923926501));
#8217=CARTESIAN_POINT('Ctrl Pts',(-0.804892650149939,-1.21345200008106,
0.000555700457907037));
#8218=CARTESIAN_POINT('Ctrl Pts',(-0.790929136238163,-1.21243049891249,
-0.237033028786364));
#8219=CARTESIAN_POINT('Ctrl Pts',(-0.776965622326388,-1.14478890768345,
-0.475158936228772));
#8220=CARTESIAN_POINT('Ctrl Pts',(-0.763002108414612,-1.01455126765528,
-0.671833688654041));
#8221=CARTESIAN_POINT('Ctrl Pts',(-0.739637062516432,-0.796625575300528,
-1.00092811620745));
#8222=CARTESIAN_POINT('Ctrl Pts',(-0.716272016618252,-0.403436676309569,
-1.21396310412447));
#8223=CARTESIAN_POINT('Ctrl Pts',(-0.692906970720071,-0.00873828951562631,
-1.21679792680243));
#8224=CARTESIAN_POINT('Ctrl Pts',(-0.66954192482189,0.385960097278319,-1.21963274948038));
#8225=CARTESIAN_POINT('Ctrl Pts',(-0.646176878923709,0.782167971875248,
-1.01226740691925));
#8226=CARTESIAN_POINT('Ctrl Pts',(-0.622811833025528,1.00479768075463,-0.686335959703516));
#8227=CARTESIAN_POINT('Ctrl Pts',(-0.599446787127348,1.22742738963402,-0.360404512487788));
#8228=CARTESIAN_POINT('Ctrl Pts',(-0.576081741229167,1.27647893279586,0.0840930393825391));
#8229=CARTESIAN_POINT('Ctrl Pts',(-0.552716695330987,1.13027577545516,0.450724490835534));
#8230=CARTESIAN_POINT('Ctrl Pts',(-0.529351649432806,0.984072618114463,
0.817355942288532));
#8231=CARTESIAN_POINT('Ctrl Pts',(-0.505986603534625,0.642614760271223,
1.1061212933242));
#8232=CARTESIAN_POINT('Ctrl Pts',(-0.482621557636444,0.256795879861456,
1.18942170363709));
#8233=CARTESIAN_POINT('Ctrl Pts',(-0.459256511738263,-0.129023000548309,
1.27272211394999));
#8234=CARTESIAN_POINT('Ctrl Pts',(-0.435891465840083,-0.559202903524601,
1.15055758354011));
#8235=CARTESIAN_POINT('Ctrl Pts',(-0.412526419941902,-0.84364432694555,
0.876896342694676));
#8236=CARTESIAN_POINT('Ctrl Pts',(-0.393315163344581,-1.07751834525735,
0.651886028504265));
#8237=CARTESIAN_POINT('Ctrl Pts',(-0.37410390674726,-1.21286598892674,0.324456492602413));
#8238=CARTESIAN_POINT('Ctrl Pts',(-0.354892650149939,-1.2156153315498,-0.000937869499410686));
#8239=CARTESIAN_POINT('Origin',(-3.06687266823562,0.,0.));
#8240=CARTESIAN_POINT('',(-0.141872668235622,-0.959049870308857,-0.000693957916149163));
#8241=CARTESIAN_POINT('',(-0.0531273317643739,-0.958113697008845,0.00104402191651295));
#8242=CARTESIAN_POINT('',(-3.06687266823562,-0.95825,-2.57321451159241E-15));
#8243=CARTESIAN_POINT('',(5.20417042793042E-17,0.382997178453078,-0.879688698994096));
#8244=CARTESIAN_POINT('Ctrl Pts',(-0.141872668235623,-0.959049870308857,
-0.000693957916149159));
#8245=CARTESIAN_POINT('Ctrl Pts',(-0.138630401878326,-0.959383036932027,
-0.0439663989064678));
#8246=CARTESIAN_POINT('Ctrl Pts',(-0.112023089622848,-0.937346021668143,
-0.398718122803486));
#8247=CARTESIAN_POINT('Ctrl Pts',(-0.064732200210974,-0.519622583613204,
-0.977168669190065));
#8248=CARTESIAN_POINT('Ctrl Pts',(-0.0206835771563966,0.129196057750057,
-0.988008553242574));
#8249=CARTESIAN_POINT('Ctrl Pts',(1.95156391047391E-17,0.382997178453079,
-0.879688698994096));
#8250=CARTESIAN_POINT('',(0.,-0.706474930361996,-0.647407317899646));
#8251=CARTESIAN_POINT('Origin',(0.,0.,0.));
#8252=CARTESIAN_POINT('Ctrl Pts',(-0.0531273317643739,-0.958113697008845,
0.00104402191651295));
#8253=CARTESIAN_POINT('Ctrl Pts',(-0.0354182211762492,-0.955989012569265,
-0.235236130484369));
#8254=CARTESIAN_POINT('Ctrl Pts',(-0.0177091105881247,-0.866556638099344,
-0.47272020794717));
#8255=CARTESIAN_POINT('Ctrl Pts',(0.,-0.706474930361996,-0.647407317899646));
#8256=CARTESIAN_POINT('Origin',(-3.06687266823562,0.,0.));
#8257=CARTESIAN_POINT('',(-0.591872668235624,-0.956887523241153,0.000272203668602481));
#8258=CARTESIAN_POINT('',(-0.503127331764375,-0.958735301611192,-0.00073968185005005));
#8259=CARTESIAN_POINT('',(-3.06687266823562,-0.95825,-2.57321451159241E-15));
#8260=CARTESIAN_POINT('Ctrl Pts',(-0.591872668235624,-0.956887523241153,
0.000272203668602485));
#8261=CARTESIAN_POINT('Ctrl Pts',(-0.578820677267412,-0.956423121808899,
-0.174943634853164));
#8262=CARTESIAN_POINT('Ctrl Pts',(-0.542403640401018,-0.827478287706606,
-0.664458216830761));
#8263=CARTESIAN_POINT('Ctrl Pts',(-0.482621557636444,-0.0510386495398221,
-1.12431386735868));
#8264=CARTESIAN_POINT('Ctrl Pts',(-0.412526419941902,0.904457501930876,
-0.669839105178461));
#8265=CARTESIAN_POINT('Ctrl Pts',(-0.342431282247359,1.06057156571601,0.37670467467911));
#8266=CARTESIAN_POINT('Ctrl Pts',(-0.272336144552818,0.279346087527691,
1.09020869981052));
#8267=CARTESIAN_POINT('Ctrl Pts',(-0.205483273215571,-0.701237154507542,
0.85191685148548));
#8268=CARTESIAN_POINT('Ctrl Pts',(-0.161995447776507,-0.956982107278429,
0.267871821167497));
#8269=CARTESIAN_POINT('Ctrl Pts',(-0.141872668235623,-0.959049870308857,
-0.000693957916149159));
#8270=CARTESIAN_POINT('Ctrl Pts',(-0.503127331764375,-0.958735301611192,
-0.000739681850050059));
#8271=CARTESIAN_POINT('Ctrl Pts',(-0.498973542463515,-0.959204136697488,
-0.0562279620506522));
#8272=CARTESIAN_POINT('Ctrl Pts',(-0.471454707264475,-0.929920724358644,
-0.423340439029663));
#8273=CARTESIAN_POINT('Ctrl Pts',(-0.420570826167254,-0.456959852937158,
-1.02848258701033));
#8274=CARTESIAN_POINT('Ctrl Pts',(-0.350475688472711,0.598427973773188,
-0.953300309276372));
#8275=CARTESIAN_POINT('Ctrl Pts',(-0.280380550778169,1.12493185591355,-0.0352038077644344));
#8276=CARTESIAN_POINT('Ctrl Pts',(-0.210285413083627,0.657167771359294,
0.913300215389848));
#8277=CARTESIAN_POINT('Ctrl Pts',(-0.140190275389085,-0.391346585807462,
1.05597004801595));
#8278=CARTESIAN_POINT('Ctrl Pts',(-0.0878042482826666,-0.916578406566786,
0.46308350348097));
#8279=CARTESIAN_POINT('Ctrl Pts',(-0.0587832670744299,-0.958792278673619,
0.0765071712587342));
#8280=CARTESIAN_POINT('Ctrl Pts',(-0.0531273317643739,-0.958113697008845,
0.00104402191651295));
#8281=CARTESIAN_POINT('Origin',(-3.06687266823562,0.,0.));
#8282=CARTESIAN_POINT('',(-1.04187266823562,-0.959673914403541,0.000115043233756074));
#8283=CARTESIAN_POINT('',(-0.953127331764375,-0.957029118582447,0.000438271575131308));
#8284=CARTESIAN_POINT('',(-3.06687266823562,-0.95825,-2.57321451159241E-15));
#8285=CARTESIAN_POINT('Ctrl Pts',(-1.04187266823562,-0.959673914403541,
0.000115043233756108));
#8286=CARTESIAN_POINT('Ctrl Pts',(-1.0190109526565,-0.959139943958945,-0.304495461135321));
#8287=CARTESIAN_POINT('Ctrl Pts',(-0.972784191179187,-0.640129375198145,
-0.921388892840649));
#8288=CARTESIAN_POINT('Ctrl Pts',(-0.903192383803697,0.402312809571003,
-1.05111767609328));
#8289=CARTESIAN_POINT('Ctrl Pts',(-0.833097246109155,1.09672346006924,-0.252788854520488));
#8290=CARTESIAN_POINT('Ctrl Pts',(-0.763002108414613,0.821830339982639,
0.76896033823534));
#8291=CARTESIAN_POINT('Ctrl Pts',(-0.69290697072007,-0.17941073460045,1.11108662859757));
#8292=CARTESIAN_POINT('Ctrl Pts',(-0.635863823993741,-0.86517647964954,
0.59036482081822));
#8293=CARTESIAN_POINT('Ctrl Pts',(-0.602185723165592,-0.95725447089627,
0.138719324240192));
#8294=CARTESIAN_POINT('Ctrl Pts',(-0.591872668235624,-0.956887523241153,
0.000272203668602485));
#8295=CARTESIAN_POINT('Ctrl Pts',(-0.953127331764375,-0.957029118582447,
0.00043827157513129));
#8296=CARTESIAN_POINT('Ctrl Pts',(-0.9391638178526,-0.956223477846001,-0.1869439504811));
#8297=CARTESIAN_POINT('Ctrl Pts',(-0.901835258042643,-0.813609242388342,
-0.689004053082304));
#8298=CARTESIAN_POINT('Ctrl Pts',(-0.841141652334508,-0.00808224906629952,
-1.12544931827059));
#8299=CARTESIAN_POINT('Ctrl Pts',(-0.771046514639964,0.929365148050997,
-0.634812677507132));
#8300=CARTESIAN_POINT('Ctrl Pts',(-0.700951376945424,1.04542352147034,0.416890480714455));
#8301=CARTESIAN_POINT('Ctrl Pts',(-0.630856239250879,0.237517367696804,
1.10012356128217));
#8302=CARTESIAN_POINT('Ctrl Pts',(-0.564914890857198,-0.719993809571971,
0.828204992971714));
#8303=CARTESIAN_POINT('Ctrl Pts',(-0.522338588361696,-0.956566941472467,
0.255893361346717));
#8304=CARTESIAN_POINT('Ctrl Pts',(-0.503127331764375,-0.958735301611192,
-0.000739681850050059));
#8305=CARTESIAN_POINT('Origin',(-3.06687266823562,0.,0.));
#8306=CARTESIAN_POINT('',(-1.49187266823562,-0.957047670170947,-0.000453923771978915));
#8307=CARTESIAN_POINT('',(-1.40312733176438,-0.959680344137663,-9.35113446810798E-5));
#8308=CARTESIAN_POINT('',(-3.06687266823562,-0.95825,-2.57321451159241E-15));
#8309=CARTESIAN_POINT('Ctrl Pts',(-1.49187266823562,-0.957047670170947,
-0.000453923771978936));
#8310=CARTESIAN_POINT('Ctrl Pts',(-1.48256627394376,-0.957605071408786,
-0.125334574811913));
#8311=CARTESIAN_POINT('Ctrl Pts',(-1.44989483375372,-0.877590088530535,
-0.563060392917903));
#8312=CARTESIAN_POINT('Ctrl Pts',(-1.39385834766549,-0.226088456349441,
-1.10253603924939));
#8313=CARTESIAN_POINT('Ctrl Pts',(-1.32376320997095,0.788684754018751,-0.802920586529807));
#8314=CARTESIAN_POINT('Ctrl Pts',(-1.25366807227641,1.10640475563864,0.206332424829975));
#8315=CARTESIAN_POINT('Ctrl Pts',(-1.18357293458187,0.446264439763658,1.03322408776754));
#8316=CARTESIAN_POINT('Ctrl Pts',(-1.11347779688732,-0.608292193570018,
0.946934534948777));
#8317=CARTESIAN_POINT('Ctrl Pts',(-1.06624437477191,-0.956629001276476,
0.324833752021017));
#8318=CARTESIAN_POINT('Ctrl Pts',(-1.04237599855468,-0.959685670455414,
0.00682143855305239));
#8319=CARTESIAN_POINT('Ctrl Pts',(-1.04187266823562,-0.959673914403541,
0.000115043233756108));
#8320=CARTESIAN_POINT('Ctrl Pts',(-1.40312733176438,-0.959680344137663,
-9.35113446812153E-5));
#8321=CARTESIAN_POINT('Ctrl Pts',(-1.40271913913987,-0.959688166301716,
-0.00553218913517348));
#8322=CARTESIAN_POINT('Ctrl Pts',(-1.37894590061717,-0.957219251541219,
-0.3222748308864));
#8323=CARTESIAN_POINT('Ctrl Pts',(-1.3318076161963,-0.612060912713934,-0.944502618736714));
#8324=CARTESIAN_POINT('Ctrl Pts',(-1.26171247850176,0.44214335137808,-1.03499442379023));
#8325=CARTESIAN_POINT('Ctrl Pts',(-1.19161734080722,1.10557358431864,-0.210739604904639));
#8326=CARTESIAN_POINT('Ctrl Pts',(-1.12152220311268,0.791878245487139,0.799770620096117));
#8327=CARTESIAN_POINT('Ctrl Pts',(-1.05142706541813,-0.22169310607518,1.10342916600544));
#8328=CARTESIAN_POINT('Ctrl Pts',(-0.995295441635367,-0.876448687134617,
0.565640378200179));
#8329=CARTESIAN_POINT('Ctrl Pts',(-0.962528863750781,-0.957571550609307,
0.126601353839102));
#8330=CARTESIAN_POINT('Ctrl Pts',(-0.953127331764375,-0.957029118582447,
0.00043827157513129));
#8331=CARTESIAN_POINT('Origin',(-3.06687266823562,0.,0.));
#8332=CARTESIAN_POINT('',(-1.94187266823562,-0.958689328197825,0.000800959330899789));
#8333=CARTESIAN_POINT('',(-1.85312733176438,-0.956897745415108,-0.00028687398796072));
#8334=CARTESIAN_POINT('',(-3.06687266823562,-0.95825,-2.57321451159241E-15));
#8335=CARTESIAN_POINT('Ctrl Pts',(-1.94187266823562,-0.958689328197825,
0.000800959330899747));
#8336=CARTESIAN_POINT('Ctrl Pts',(-1.92275654933285,-0.956519486288093,
-0.254585784224982));
#8337=CARTESIAN_POINT('Ctrl Pts',(-1.88027538453189,-0.721924785019282,
-0.825806756370372));
#8338=CARTESIAN_POINT('Ctrl Pts',(-1.81442917383274,0.233140677181374,-1.1010152907217));
#8339=CARTESIAN_POINT('Ctrl Pts',(-1.74433403613821,1.04374906965657,-0.421077590856424));
#8340=CARTESIAN_POINT('Ctrl Pts',(-1.67423889844366,0.931890207415111,0.631116820366198));
#8341=CARTESIAN_POINT('Ctrl Pts',(-1.60414376074912,-0.00359849674038535,
1.12546597767462));
#8342=CARTESIAN_POINT('Ctrl Pts',(-1.54335501734644,-0.812122043604567,
0.691564032716878));
#8343=CARTESIAN_POINT('Ctrl Pts',(-1.50593131984194,-0.956205635161259,
0.188196321455179));
#8344=CARTESIAN_POINT('Ctrl Pts',(-1.49187266823562,-0.957047670170947,
-0.000453923771978936));
#8345=CARTESIAN_POINT('Ctrl Pts',(-1.85312733176438,-0.956897745415108,
-0.000286873987960694));
#8346=CARTESIAN_POINT('Ctrl Pts',(-1.84290941452895,-0.957286680280528,
-0.137455108397305));
#8347=CARTESIAN_POINT('Ctrl Pts',(-1.80932645139534,-0.866385265055213,
-0.587793994348256));
#8348=CARTESIAN_POINT('Ctrl Pts',(-1.75237844236356,-0.183834647990358,
-1.1103563267006));
#8349=CARTESIAN_POINT('Ctrl Pts',(-1.68228330466901,0.818758071214107,-0.772232628794933));
#8350=CARTESIAN_POINT('Ctrl Pts',(-1.61218816697447,1.09772272845902,0.248418045560514));
#8351=CARTESIAN_POINT('Ctrl Pts',(-1.54209302927993,0.406498045477112,1.04950504037332));
#8352=CARTESIAN_POINT('Ctrl Pts',(-1.4724060842099,-0.637878025349449,0.923761319253053));
#8353=CARTESIAN_POINT('Ctrl Pts',(-1.42608418503805,-0.959240423713628,
0.30577906092175));
#8354=CARTESIAN_POINT('Ctrl Pts',(-1.40312733176438,-0.959680344137663,
-9.35113446812153E-5));
#8355=CARTESIAN_POINT('Ctrl Pts',(-2.38323468161444,-0.418777734803984,
0.861898063191027));
#8356=CARTESIAN_POINT('Ctrl Pts',(-2.35986963571626,-0.699961277147284,
0.725277026486611));
#8357=CARTESIAN_POINT('Ctrl Pts',(-2.3131395439199,-1.11403436160083,0.158253196261579));
#8358=CARTESIAN_POINT('Ctrl Pts',(-2.24304440622535,-0.752359592709721,
-0.837961774657783));
#8359=CARTESIAN_POINT('Ctrl Pts',(-2.17294926853081,0.275115309926484,-1.09100794194568));
#8360=CARTESIAN_POINT('Ctrl Pts',(-2.10285413083626,1.05900093864512,-0.381087916994184));
#8361=CARTESIAN_POINT('Ctrl Pts',(-2.03275899314173,0.907151642232085,0.666313302776059));
#8362=CARTESIAN_POINT('Ctrl Pts',(-1.96266385544718,-0.0465745614418721,
1.12446411646007));
#8363=CARTESIAN_POINT('Ctrl Pts',(-1.89256871775265,-0.959074148548053,
0.588978031955627));
#8364=CARTESIAN_POINT('Ctrl Pts',(-1.8224735800581,-1.02396023446961,-0.467154233019447));
#8365=CARTESIAN_POINT('Ctrl Pts',(-1.75237844236356,-0.183834647990358,
-1.1103563267006));
#8366=CARTESIAN_POINT('Ctrl Pts',(-1.68228330466901,0.818758071214107,-0.772232628794933));
#8367=CARTESIAN_POINT('Ctrl Pts',(-1.61218816697447,1.09772272845902,0.248418045560514));
#8368=CARTESIAN_POINT('Ctrl Pts',(-1.54209302927993,0.406498045477112,1.04950504037332));
#8369=CARTESIAN_POINT('Ctrl Pts',(-1.47199789158539,-0.643995478322856,
0.923024772981895));
#8370=CARTESIAN_POINT('Ctrl Pts',(-1.40190275389085,-1.12531508782357,-0.0192431825357103));
#8371=CARTESIAN_POINT('Ctrl Pts',(-1.3318076161963,-0.612060912713934,-0.944502618736714));
#8372=CARTESIAN_POINT('Ctrl Pts',(-1.26171247850176,0.44214335137808,-1.03499442379023));
#8373=CARTESIAN_POINT('Ctrl Pts',(-1.19161734080722,1.10557358431864,-0.210739604904639));
#8374=CARTESIAN_POINT('Ctrl Pts',(-1.12152220311268,0.791878245487139,0.799770620096117));
#8375=CARTESIAN_POINT('Ctrl Pts',(-1.05142706541813,-0.22169310607518,1.10342916600544));
#8376=CARTESIAN_POINT('Ctrl Pts',(-0.981331927723592,-1.03932814881416,
0.431858016065468));
#8377=CARTESIAN_POINT('Ctrl Pts',(-0.911236790029049,-0.938386600814667,
-0.621398016612586));
#8378=CARTESIAN_POINT('Ctrl Pts',(-0.841141652334508,-0.00808224906629952,
-1.12544931827059));
#8379=CARTESIAN_POINT('Ctrl Pts',(-0.771046514639964,0.929365148050997,
-0.634812677507132));
#8380=CARTESIAN_POINT('Ctrl Pts',(-0.700951376945424,1.04542352147034,0.416890480714455));
#8381=CARTESIAN_POINT('Ctrl Pts',(-0.630856239250879,0.237517367696804,
1.10012356128217));
#8382=CARTESIAN_POINT('Ctrl Pts',(-0.560761101556339,-0.780309526197106,
0.811076249516093));
#8383=CARTESIAN_POINT('Ctrl Pts',(-0.490665963861796,-1.10848754091122,
-0.194868458669156));
#8384=CARTESIAN_POINT('Ctrl Pts',(-0.420570826167254,-0.456959852937158,
-1.02848258701033));
#8385=CARTESIAN_POINT('Ctrl Pts',(-0.350475688472711,0.598427973773188,
-0.953300309276372));
#8386=CARTESIAN_POINT('Ctrl Pts',(-0.280380550778169,1.12493185591355,-0.0352038077644344));
#8387=CARTESIAN_POINT('Ctrl Pts',(-0.210285413083627,0.657167771359294,
0.913300215389848));
#8388=CARTESIAN_POINT('Ctrl Pts',(-0.140190275389085,-0.391346585807462,
1.05597004801595));
#8389=CARTESIAN_POINT('Ctrl Pts',(-0.0700951376945419,-1.09413316519229,
0.262658047241422));
#8390=CARTESIAN_POINT('Ctrl Pts',(-0.0233650458981807,-0.917683530033312,
-0.416928643008026));
#8391=CARTESIAN_POINT('Ctrl Pts',(0.,-0.706474930361996,-0.647407317899646));
#8392=CARTESIAN_POINT('Ctrl Pts',(-2.33382312107629,-0.456179659636029,
0.938876001350623));
#8393=CARTESIAN_POINT('Ctrl Pts',(-2.31045807517811,-0.762476298595258,
0.790053051028027));
#8394=CARTESIAN_POINT('Ctrl Pts',(-2.26372798338175,-1.21353112561197,0.172387123782289));
#8395=CARTESIAN_POINT('Ctrl Pts',(-2.19363284568721,-0.819554418495693,
-0.912801912284841));
#8396=CARTESIAN_POINT('Ctrl Pts',(-2.12353770799266,0.299686439876436,-1.18844816773733));
#8397=CARTESIAN_POINT('Ctrl Pts',(-2.05344257029812,1.15358255130609,-0.415123684517711));
#8398=CARTESIAN_POINT('Ctrl Pts',(-1.98334743260358,0.988171273206288,0.725823152497863));
#8399=CARTESIAN_POINT('Ctrl Pts',(-1.91325229490904,-0.0507342339873809,
1.22489238392719));
#8400=CARTESIAN_POINT('Ctrl Pts',(-1.84315715721449,-1.04473108833054,0.641580905146204));
#8401=CARTESIAN_POINT('Ctrl Pts',(-1.77306201951995,-1.11541228776122,-0.50887676517972));
#8402=CARTESIAN_POINT('Ctrl Pts',(-1.70296688182541,-0.200253309046633,
-1.20952459763907));
#8403=CARTESIAN_POINT('Ctrl Pts',(-1.63287174413087,0.891883085488123,-0.841202357447199));
#8404=CARTESIAN_POINT('Ctrl Pts',(-1.56277660643633,1.19576266602989,0.270604786389338));
#8405=CARTESIAN_POINT('Ctrl Pts',(-1.49268146874178,0.442803245294923,1.14323855428439));
#8406=CARTESIAN_POINT('Ctrl Pts',(-1.42258633104724,-0.701512075960701,
1.0054620668207));
#8407=CARTESIAN_POINT('Ctrl Pts',(-1.3524911933527,-1.22581935734221,-0.0209618318499275));
#8408=CARTESIAN_POINT('Ctrl Pts',(-1.28239605565816,-0.66672536678448,-1.02885814438612));
#8409=CARTESIAN_POINT('Ctrl Pts',(-1.21230091796362,0.481632108823535,-1.12743196385742));
#8410=CARTESIAN_POINT('Ctrl Pts',(-1.14220578026907,1.2043146984238,-0.229561204542612));
#8411=CARTESIAN_POINT('Ctrl Pts',(-1.07211064257453,0.862602565698921,0.871199824969472));
#8412=CARTESIAN_POINT('Ctrl Pts',(-1.00201550487999,-0.241492986059457,
1.20197875757754));
#8413=CARTESIAN_POINT('Ctrl Pts',(-0.931920367185445,-1.13215274302515,
0.470428168469959));
#8414=CARTESIAN_POINT('Ctrl Pts',(-0.861825229490904,-1.02219589197361,
-0.676896387171863));
#8415=CARTESIAN_POINT('Ctrl Pts',(-0.791730091796362,-0.00880409181707018,
-1.22596557619423));
#8416=CARTESIAN_POINT('Ctrl Pts',(-0.721634954101819,1.01236871419139,-0.691509139790793));
#8417=CARTESIAN_POINT('Ctrl Pts',(-0.651539816407278,1.13879250629946,0.454123850893925));
#8418=CARTESIAN_POINT('Ctrl Pts',(-0.581444678712735,0.258730545940533,
1.19837792230807));
#8419=CARTESIAN_POINT('Ctrl Pts',(-0.511349541018193,-0.850000619631704,
0.883515184054141));
#8420=CARTESIAN_POINT('Ctrl Pts',(-0.44125440332365,-1.20748890664005,-0.212272572683697));
#8421=CARTESIAN_POINT('Ctrl Pts',(-0.371159265629109,-0.497771903460376,
-1.12033854116805));
#8422=CARTESIAN_POINT('Ctrl Pts',(-0.301064127934566,0.651874841245582,
-1.03844157526705));
#8423=CARTESIAN_POINT('Ctrl Pts',(-0.230968990240023,1.22540189818011,-0.0383479342601363));
#8424=CARTESIAN_POINT('Ctrl Pts',(-0.160873852545481,0.715860814335727,
0.994868988431449));
#8425=CARTESIAN_POINT('Ctrl Pts',(-0.090778714850939,-0.426298576730522,
1.15028096542724));
#8426=CARTESIAN_POINT('Ctrl Pts',(-0.0206835771563966,-1.19185251127912,
0.286116592725112));
#8427=CARTESIAN_POINT('Ctrl Pts',(0.0260465146399647,-0.999643786172473,
-0.454165421542616));
#8428=CARTESIAN_POINT('Ctrl Pts',(0.0494115605381454,-0.769571699949071,
-0.705228634143052));
#8429=CARTESIAN_POINT('Ctrl Pts',(-2.28441156053815,-0.493581584468075,
1.01585393951022));
#8430=CARTESIAN_POINT('Ctrl Pts',(-2.26104651463996,-0.824991320043233,
0.854829075569444));
#8431=CARTESIAN_POINT('Ctrl Pts',(-2.21431642284361,-1.3130278896231,0.186521051302999));
#8432=CARTESIAN_POINT('Ctrl Pts',(-2.14422128514906,-0.886749244281665,
-0.987642049911899));
#8433=CARTESIAN_POINT('Ctrl Pts',(-2.07412614745452,0.324257569826388,-1.28588839352898));
#8434=CARTESIAN_POINT('Ctrl Pts',(-2.00403100975997,1.24816416396707,-0.449159452041237));
#8435=CARTESIAN_POINT('Ctrl Pts',(-1.93393587206544,1.06919090418049,0.785333002219665));
#8436=CARTESIAN_POINT('Ctrl Pts',(-1.86384073437089,-0.0548939065328899,
1.32532065139432));
#8437=CARTESIAN_POINT('Ctrl Pts',(-1.79374559667635,-1.13038802811303,0.694183778336778));
#8438=CARTESIAN_POINT('Ctrl Pts',(-1.7236504589818,-1.20686434105284,-0.550599297339992));
#8439=CARTESIAN_POINT('Ctrl Pts',(-1.65355532128727,-0.216671970102907,
-1.30869286857755));
#8440=CARTESIAN_POINT('Ctrl Pts',(-1.58346018359272,0.965008099762136,-0.910172086099464));
#8441=CARTESIAN_POINT('Ctrl Pts',(-1.51336504589818,1.29380260360076,0.292791527218161));
#8442=CARTESIAN_POINT('Ctrl Pts',(-1.44326990820364,0.479108445112733,1.23697206819546));
#8443=CARTESIAN_POINT('Ctrl Pts',(-1.3731747705091,-0.759028673598546,1.0878993606595));
#8444=CARTESIAN_POINT('Ctrl Pts',(-1.30307963281456,-1.32632362686085,-0.0226804811641433));
#8445=CARTESIAN_POINT('Ctrl Pts',(-1.23298449512001,-0.721389820855027,
-1.11321367003554));
#8446=CARTESIAN_POINT('Ctrl Pts',(-1.16288935742547,0.52112086626899,-1.21986950392461));
#8447=CARTESIAN_POINT('Ctrl Pts',(-1.09279421973093,1.30305581252896,-0.248382804180586));
#8448=CARTESIAN_POINT('Ctrl Pts',(-1.02269908203639,0.933326885910705,0.942629029842827));
#8449=CARTESIAN_POINT('Ctrl Pts',(-0.952603944341841,-0.261292866043736,
1.30052834914964));
#8450=CARTESIAN_POINT('Ctrl Pts',(-0.882508806647302,-1.22497733723614,
0.50899832087445));
#8451=CARTESIAN_POINT('Ctrl Pts',(-0.812413668952757,-1.10600518313255,
-0.73239475773114));
#8452=CARTESIAN_POINT('Ctrl Pts',(-0.742318531258218,-0.00952593456783798,
-1.32648183411787));
#8453=CARTESIAN_POINT('Ctrl Pts',(-0.672223393563673,1.09537228033178,-0.748205602074454));
#8454=CARTESIAN_POINT('Ctrl Pts',(-0.602128255869133,1.23216149112858,0.491357221073396));
#8455=CARTESIAN_POINT('Ctrl Pts',(-0.532033118174589,0.27994372418426,1.29663228333396));
#8456=CARTESIAN_POINT('Ctrl Pts',(-0.461937980480048,-0.919691713066301,
0.955954118592191));
#8457=CARTESIAN_POINT('Ctrl Pts',(-0.391842842785505,-1.30649027236888,
-0.22967668669824));
#8458=CARTESIAN_POINT('Ctrl Pts',(-0.321747705090963,-0.538583953983592,
-1.21219449532577));
#8459=CARTESIAN_POINT('Ctrl Pts',(-0.251652567396421,0.705321708717977,
-1.12358284125773));
#8460=CARTESIAN_POINT('Ctrl Pts',(-0.181557429701878,1.32587194044667,-0.041492060755839));
#8461=CARTESIAN_POINT('Ctrl Pts',(-0.111462292007336,0.774553857312159,
1.07643776147305));
#8462=CARTESIAN_POINT('Ctrl Pts',(-0.0413671543127934,-0.461250567653581,
1.24459188283852));
#8463=CARTESIAN_POINT('Ctrl Pts',(0.0287279833817485,-1.28957185736595,
0.309575138208801));
#8464=CARTESIAN_POINT('Ctrl Pts',(0.0754580751781104,-1.08160404231163,
-0.491402200077204));
#8465=CARTESIAN_POINT('Ctrl Pts',(0.098823121076291,-0.832668469536145,
-0.763049950386459));
#8466=CARTESIAN_POINT('Ctrl Pts',(-2.235,-0.53098350930012,1.09283187766981));
#8467=CARTESIAN_POINT('Ctrl Pts',(-2.21163495410182,-0.887506341491207,
0.919605100110861));
#8468=CARTESIAN_POINT('Ctrl Pts',(-2.16490486230546,-1.41252465363424,0.200654978823709));
#8469=CARTESIAN_POINT('Ctrl Pts',(-2.09480972461092,-0.953944070067637,
-1.06248218753896));
#8470=CARTESIAN_POINT('Ctrl Pts',(-2.02471458691637,0.34882869977634,-1.38332861932063));
#8471=CARTESIAN_POINT('Ctrl Pts',(-1.95461944922183,1.34274577662804,-0.483195219564764));
#8472=CARTESIAN_POINT('Ctrl Pts',(-1.88452431152729,1.15021053515469,0.844842851941468));
#8473=CARTESIAN_POINT('Ctrl Pts',(-1.81442917383275,-0.0590535790783977,
1.42574891886144));
#8474=CARTESIAN_POINT('Ctrl Pts',(-1.7443340361382,-1.21604496789552,0.746786651527355));
#8475=CARTESIAN_POINT('Ctrl Pts',(-1.67423889844366,-1.29831639434446,-0.592321829500264));
#8476=CARTESIAN_POINT('Ctrl Pts',(-1.60414376074912,-0.233090631159182,
-1.40786113951602));
#8477=CARTESIAN_POINT('Ctrl Pts',(-1.53404862305458,1.03813311403615,-0.979141814751728));
#8478=CARTESIAN_POINT('Ctrl Pts',(-1.46395348536003,1.39184254117163,0.314978268046985));
#8479=CARTESIAN_POINT('Ctrl Pts',(-1.3938583476655,0.515413644930542,1.33070558210653));
#8480=CARTESIAN_POINT('Ctrl Pts',(-1.32376320997095,-0.816545271236388,
1.17033665449831));
#8481=CARTESIAN_POINT('Ctrl Pts',(-1.25366807227641,-1.42682789637949,-0.0243991304783595));
#8482=CARTESIAN_POINT('Ctrl Pts',(-1.18357293458187,-0.776054274925573,
-1.19756919568495));
#8483=CARTESIAN_POINT('Ctrl Pts',(-1.11347779688733,0.560609623714444,-1.31230704399179));
#8484=CARTESIAN_POINT('Ctrl Pts',(-1.04338265919278,1.40179692663412,-0.267204403818561));
#8485=CARTESIAN_POINT('Ctrl Pts',(-0.97328752149824,1.00405120612249,1.01405823471618));
#8486=CARTESIAN_POINT('Ctrl Pts',(-0.903192383803698,-0.281092746028013,
1.39907794072174));
#8487=CARTESIAN_POINT('Ctrl Pts',(-0.833097246109156,-1.31780193144713,
0.547568473278941));
#8488=CARTESIAN_POINT('Ctrl Pts',(-0.763002108414612,-1.18981447429149,
-0.787893128290417));
#8489=CARTESIAN_POINT('Ctrl Pts',(-0.692906970720072,-0.0102477773186068,
-1.4269980920415));
#8490=CARTESIAN_POINT('Ctrl Pts',(-0.622811833025528,1.17837584647217,-0.804902064358118));
#8491=CARTESIAN_POINT('Ctrl Pts',(-0.552716695330987,1.3255304759577,0.528590591252869));
#8492=CARTESIAN_POINT('Ctrl Pts',(-0.482621557636444,0.301156902427986,
1.39488664435986));
#8493=CARTESIAN_POINT('Ctrl Pts',(-0.412526419941902,-0.989382806500896,
1.02839305313024));
#8494=CARTESIAN_POINT('Ctrl Pts',(-0.342431282247359,-1.40549163809771,
-0.247080800712783));
#8495=CARTESIAN_POINT('Ctrl Pts',(-0.272336144552818,-0.579396004506808,
-1.30405044948349));
#8496=CARTESIAN_POINT('Ctrl Pts',(-0.202241006858275,0.75876857619037,-1.20872410724841));
#8497=CARTESIAN_POINT('Ctrl Pts',(-0.132145869163733,1.42634198271324,-0.0446361872515408));
#8498=CARTESIAN_POINT('Ctrl Pts',(-0.0620507314691905,0.833246900288591,
1.15800653451465));
#8499=CARTESIAN_POINT('Ctrl Pts',(0.00804440622535185,-0.49620255857664,
1.33890280024981));
#8500=CARTESIAN_POINT('Ctrl Pts',(0.0781395439198939,-1.38729120345278,
0.333033683692492));
#8501=CARTESIAN_POINT('Ctrl Pts',(0.124869635716256,-1.1635642984508,-0.528638978611794));
#8502=CARTESIAN_POINT('Ctrl Pts',(0.148234681614436,-0.89576523912322,-0.820871266629866));
#8503=CARTESIAN_POINT('',(0.,-0.292167722185243,1.17934855836309));
#8504=CARTESIAN_POINT('Ctrl Pts',(-3.05311331771918E-16,-0.293132536858745,
1.18067345457));
#8505=CARTESIAN_POINT('Ctrl Pts',(-2.41399024079808E-16,-0.335932013416244,
1.16561322977037));
#8506=CARTESIAN_POINT('Ctrl Pts',(-3.24049613596376E-16,-0.377726074145918,
1.14807981448758));
#8507=CARTESIAN_POINT('Ctrl Pts',(-1.66533453693773E-16,-0.418289929981307,
1.12802261826284));
#8508=CARTESIAN_POINT('Ctrl Pts',(-4.17758082892349E-18,-0.460100117742301,
1.10734916099787));
#8509=CARTESIAN_POINT('Ctrl Pts',(-2.2251679718906E-16,-0.500603870175662,
1.08399372536458));
#8510=CARTESIAN_POINT('Ctrl Pts',(5.55111512312578E-17,-0.539635460376147,
1.05816525512961));
#8511=CARTESIAN_POINT('Ctrl Pts',(1.43120952673795E-16,-0.551934762971012,
1.05002640735655));
#8512=CARTESIAN_POINT('Ctrl Pts',(-2.97792580155581E-16,-0.564087662460813,
1.04164182529709));
#8513=CARTESIAN_POINT('Ctrl Pts',(-3.05311331771918E-16,-0.576088318506723,
1.03301762701505));
#8514=CARTESIAN_POINT('Ctrl Pts',(-3.10957770648654E-16,-0.585100582018225,
1.02654101880331));
#8515=CARTESIAN_POINT('Ctrl Pts',(-1.87805466987078E-17,-0.594018974805992,
1.01993501166421));
#8516=CARTESIAN_POINT('Ctrl Pts',(0.,-0.602840687031429,1.01320339714505));
#8517=CARTESIAN_POINT('Ctrl Pts',(8.43077134695688E-17,-0.642442217196913,
0.982984520284144));
#8518=CARTESIAN_POINT('Ctrl Pts',(1.70451744334007E-16,-0.680104775291499,
0.950232561947544));
#8519=CARTESIAN_POINT('Ctrl Pts',(2.4980018054066E-16,-0.715630523030677,
0.915211265061402));
#8520=CARTESIAN_POINT('Ctrl Pts',(3.00087345968065E-16,-0.738145007737591,
0.893016476680078));
#8521=CARTESIAN_POINT('Ctrl Pts',(-1.41299001724718E-16,-0.759800462521797,
0.869909521470008));
#8522=CARTESIAN_POINT('Ctrl Pts',(-1.80411241501588E-16,-0.780536780376596,
0.845952761453801));
#8523=CARTESIAN_POINT('Ctrl Pts',(-1.95118881290929E-16,-0.788334398086693,
0.836944139118487));
#8524=CARTESIAN_POINT('Ctrl Pts',(-2.53267376952506E-16,-0.796001963266571,
0.827815325827747));
#8525=CARTESIAN_POINT('Ctrl Pts',(-3.19189119579733E-16,-0.803535968281199,
0.818569564500166));
#8526=CARTESIAN_POINT('Ctrl Pts',(-3.72764038404646E-16,-0.809658890567517,
0.811055489585601));
#8527=CARTESIAN_POINT('Ctrl Pts',(-2.69654453316991E-16,-0.815687771317065,
0.803471295609831));
#8528=CARTESIAN_POINT('Ctrl Pts',(-2.63677968348475E-16,-0.821620162866385,
0.795820485137319));
#8529=CARTESIAN_POINT('Ctrl Pts',(-2.3278733475951E-16,-0.852282890978593,
0.756275772114527));
#8530=CARTESIAN_POINT('Ctrl Pts',(-7.56686568098375E-16,-0.880382544762949,
0.714940607813026));
#8531=CARTESIAN_POINT('Ctrl Pts',(-6.80011602582908E-16,-0.905714588462527,
0.672080427349177));
#8532=CARTESIAN_POINT('Ctrl Pts',(-6.07721418114474E-16,-0.929597978558549,
0.631671275140858));
#8533=CARTESIAN_POINT('Ctrl Pts',(-1.03226703790935E-15,-0.951021292098657,
0.589905394894723));
#8534=CARTESIAN_POINT('Ctrl Pts',(-1.19348975147204E-15,-0.969765382003686,
0.546993657372317));
#8535=CARTESIAN_POINT('Ctrl Pts',(-1.28143536432127E-15,-0.979990122907564,
0.523585671168403));
#8536=CARTESIAN_POINT('Ctrl Pts',(-1.63505974646731E-16,-0.989416779428147,
0.499836614874287));
#8537=CARTESIAN_POINT('Ctrl Pts',(-1.11022302462516E-16,-0.998003181165185,
0.475780845045036));
#8538=CARTESIAN_POINT('Ctrl Pts',(-8.67220820234133E-17,-1.00197873101346,
0.464642895176907));
#8539=CARTESIAN_POINT('Ctrl Pts',(-6.74696253167536E-17,-1.00577408346956,
0.453439201601946));
#8540=CARTESIAN_POINT('Ctrl Pts',(-1.38777878078145E-17,-1.00938468801266,
0.442173233161444));
#8541=CARTESIAN_POINT('Ctrl Pts',(2.2221827891663E-17,-1.01181680160509,
0.434584444456137));
#8542=CARTESIAN_POINT('Ctrl Pts',(4.18926510052434E-16,-1.01416437175746,
0.42696939985124));
#8543=CARTESIAN_POINT('Ctrl Pts',(3.88578058618805E-16,-1.01642375179121,
0.419337791015749));
#8544=CARTESIAN_POINT('Ctrl Pts',(2.15396781121084E-16,-1.02931674310096,
0.37578855851591));
#8545=CARTESIAN_POINT('Ctrl Pts',(-6.59408752454894E-16,-1.03936791753624,
0.331620664795643));
#8546=CARTESIAN_POINT('Ctrl Pts',(-4.85722573273506E-16,-1.04638812315296,
0.287033942557984));
#8547=CARTESIAN_POINT('Ctrl Pts',(-4.42257175970882E-16,-1.04814494702758,
0.275876004686269));
#8548=CARTESIAN_POINT('Ctrl Pts',(4.37223924785986E-16,-1.04971169924956,
0.264691828952297));
#8549=CARTESIAN_POINT('Ctrl Pts',(3.88578058618805E-16,-1.05108489580466,
0.253484558391007));
#8550=CARTESIAN_POINT('Ctrl Pts',(2.4955770282928E-16,-1.05614503746883,
0.212186481653198));
#8551=CARTESIAN_POINT('Ctrl Pts',(1.34271465327458E-16,-1.05857941169269,
0.17057393394923));
#8552=CARTESIAN_POINT('Ctrl Pts',(1.87350135405495E-16,-1.05845449697657,
0.128862808641984));
#8553=CARTESIAN_POINT('Ctrl Pts',(2.13130568122753E-16,-1.05839382561028,
0.108603618689342));
#8554=CARTESIAN_POINT('Ctrl Pts',(3.52349314273582E-16,-1.05772891141692,
0.0883213386068555));
#8555=CARTESIAN_POINT('Ctrl Pts',(3.05311331771918E-16,-1.05646479410987,
0.0680420226442946));
#8556=CARTESIAN_POINT('Ctrl Pts',(2.77282717210464E-16,-1.0557115420596,
0.0559581470090151));
#8557=CARTESIAN_POINT('Ctrl Pts',(2.72979455253999E-16,-1.05474550432587,
0.0438753433176231));
#8558=CARTESIAN_POINT('Ctrl Pts',(2.35922392732846E-16,-1.0535674917508,
0.031799326129942));
#8559=CARTESIAN_POINT('Ctrl Pts',(2.11048989273273E-16,-1.0527767873596,
0.0236936742714747));
#8560=CARTESIAN_POINT('Ctrl Pts',(6.13180887324493E-16,-1.05189085250313,
0.0155945609871946));
#8561=CARTESIAN_POINT('Ctrl Pts',(6.03683769639929E-16,-1.05091130462964,
0.00751183891852238));
#8562=CARTESIAN_POINT('Ctrl Pts',(5.51080620478412E-16,-1.045485731881,
-0.0372571792963943));
#8563=CARTESIAN_POINT('Ctrl Pts',(8.13451426044107E-16,-1.0371851023245,
-0.0816002357585725));
#8564=CARTESIAN_POINT('Ctrl Pts',(7.56339435525888E-16,-1.02611974514107,
-0.125246436326617));
#8565=CARTESIAN_POINT('Ctrl Pts',(6.99580607089161E-16,-1.01512281254834,
-0.16862274290389));
#8566=CARTESIAN_POINT('Ctrl Pts',(-3.72450892574497E-16,-1.0013945728171,
-0.211311849734376));
#8567=CARTESIAN_POINT('Ctrl Pts',(-5.41233724504764E-16,-0.98499986230162,
-0.253021432803562));
#8568=CARTESIAN_POINT('Ctrl Pts',(-6.17890265177582E-16,-0.977553833703354,
-0.27196478334712));
#8569=CARTESIAN_POINT('Ctrl Pts',(-2.71631770704439E-16,-0.969557250286352,
-0.290705625787388));
#8570=CARTESIAN_POINT('Ctrl Pts',(-3.2612801348364E-16,-0.9610137551908,
-0.309213868158789));
#8571=CARTESIAN_POINT('Ctrl Pts',(-3.57229340238859E-16,-0.956137932215719,
-0.319776631099897));
#8572=CARTESIAN_POINT('Ctrl Pts',(-2.54857688098412E-16,-0.951083951554496,
-0.330263600398875));
#8573=CARTESIAN_POINT('Ctrl Pts',(-2.74086309204336E-16,-0.945852299939878,
-0.34066888161227));
#8574=CARTESIAN_POINT('Ctrl Pts',(-2.91171668308026E-16,-0.941203779068372,
-0.349914368593704));
#8575=CARTESIAN_POINT('Ctrl Pts',(-5.05212835795718E-16,-0.93641387616655,
-0.359097063515204));
#8576=CARTESIAN_POINT('Ctrl Pts',(-4.71844785465692E-16,-0.931494000461812,
-0.368193095666921));
#8577=CARTESIAN_POINT('Ctrl Pts',(-3.32738396632977E-16,-0.910983777778045,
-0.406113087180272));
#8578=CARTESIAN_POINT('Ctrl Pts',(2.09944366161902E-16,-0.888179681046059,
-0.442608221198496));
#8579=CARTESIAN_POINT('Ctrl Pts',(8.32667268468867E-17,-0.863152994506025,
-0.477421131302607));
#8580=CARTESIAN_POINT('Ctrl Pts',(-3.89291622173031E-17,-0.839011731465234,
-0.511002389400613));
#8581=CARTESIAN_POINT('Ctrl Pts',(3.08915620636759E-16,-0.81280165934355,
-0.54301893377654));
#8582=CARTESIAN_POINT('Ctrl Pts',(4.23272528138341E-16,-0.784558442664854,
-0.57320193611465));
#8583=CARTESIAN_POINT('Ctrl Pts',(5.22476258772195E-16,-0.760057671169367,
-0.599385456630273));
#8584=CARTESIAN_POINT('Ctrl Pts',(8.10803150113927E-17,-0.734026249237344,
-0.624188862340296));
#8585=CARTESIAN_POINT('Ctrl Pts',(1.38777878078145E-17,-0.706474930361996,
-0.647407317899646));
#8586=CARTESIAN_POINT('Ctrl Pts',(-0.354892650149939,-1.2156153315498,-0.000937869499410686));
#8587=CARTESIAN_POINT('Ctrl Pts',(-0.350738860849079,-1.21620978459426,
-0.0712934765369628));
#8588=CARTESIAN_POINT('Ctrl Pts',(-0.346585071548219,-1.21060532749883,
-0.14155394012693));
#8589=CARTESIAN_POINT('Ctrl Pts',(-0.342431282247359,-1.19845756056642,
-0.210663433200738));
#8590=CARTESIAN_POINT('Ctrl Pts',(-0.319066236349179,-1.13012642690074,
-0.599404016969691));
#8591=CARTESIAN_POINT('Ctrl Pts',(-0.295701190450998,-0.854761215703772,
-0.951727233226591));
#8592=CARTESIAN_POINT('Ctrl Pts',(-0.272336144552818,-0.494051179989093,
-1.11200111764919));
#8593=CARTESIAN_POINT('Ctrl Pts',(-0.248971098654637,-0.133341144274414,
-1.2722750020718));
#8594=CARTESIAN_POINT('Ctrl Pts',(-0.225606052756456,0.312713715957976,
-1.24049955466011));
#8595=CARTESIAN_POINT('Ctrl Pts',(-0.202241006858275,0.64700338049465,-1.03059717762145));
#8596=CARTESIAN_POINT('Ctrl Pts',(-0.178875960960094,0.981293045031325,
-0.82069480058279));
#8597=CARTESIAN_POINT('Ctrl Pts',(-0.155510915061913,1.20381751387228,-0.432665493917164));
#8598=CARTESIAN_POINT('Ctrl Pts',(-0.132145869163732,1.21623056788865,-0.0382103869566515));
#8599=CARTESIAN_POINT('Ctrl Pts',(-0.108780823265552,1.22864362190502,0.356244720003858));
#8600=CARTESIAN_POINT('Ctrl Pts',(-0.0854157773673712,1.03094526109681,
0.757125627259254));
#8601=CARTESIAN_POINT('Ctrl Pts',(-0.0620507314691906,0.710521170881829,
0.987715458509478));
#8602=CARTESIAN_POINT('Ctrl Pts',(-0.0413671543127939,0.426870266808673,
1.19184185256531));
#8603=CARTESIAN_POINT('Ctrl Pts',(-0.0206835771563971,0.0470462558057122,
1.26252090887865));
#8604=CARTESIAN_POINT('Ctrl Pts',(-2.94902990916057E-16,-0.293132536858746,
1.18067345457));
#8605=CARTESIAN_POINT('',(-2.235,-0.557525174626851,-0.780836043637726));
#8606=CARTESIAN_POINT('Ctrl Pts',(-2.235,-0.557525174626855,-0.780836043637723));
#8607=CARTESIAN_POINT('Ctrl Pts',(-2.235,-0.589761389590488,-0.763902150685921));
#8608=CARTESIAN_POINT('Ctrl Pts',(-2.235,-0.620887948635336,-0.745102743152277));
#8609=CARTESIAN_POINT('Ctrl Pts',(-2.235,-0.650719001081195,-0.724483598080833));
#8610=CARTESIAN_POINT('Ctrl Pts',(-2.235,-0.686232768596372,-0.699936575284436));
#8611=CARTESIAN_POINT('Ctrl Pts',(-2.235,-0.719912199030247,-0.672812168345133));
#8612=CARTESIAN_POINT('Ctrl Pts',(-2.235,-0.75168110876748,-0.643417830155717));
#8613=CARTESIAN_POINT('Ctrl Pts',(-2.235,-0.762057019880621,-0.633817467952367));
#8614=CARTESIAN_POINT('Ctrl Pts',(-2.235,-0.772232353877974,-0.623970750017659));
#8615=CARTESIAN_POINT('Ctrl Pts',(-2.235,-0.782182525354984,-0.613909717043614));
#8616=CARTESIAN_POINT('Ctrl Pts',(-2.235,-0.812598374920379,-0.583154984211313));
#8617=CARTESIAN_POINT('Ctrl Pts',(-2.235,-0.840948417922223,-0.550370430406235));
#8618=CARTESIAN_POINT('Ctrl Pts',(-2.235,-0.867164276315998,-0.515863413535596));
#8619=CARTESIAN_POINT('Ctrl Pts',(-2.235,-0.885307489374087,-0.491982137184495));
#8620=CARTESIAN_POINT('Ctrl Pts',(-2.235,-0.90242815802142,-0.467274692073097));
#8621=CARTESIAN_POINT('Ctrl Pts',(-2.235,-0.91849637257373,-0.441830457957078));
#8622=CARTESIAN_POINT('Ctrl Pts',(-2.235,-0.92388138647726,-0.433303215926959));
#8623=CARTESIAN_POINT('Ctrl Pts',(-2.235,-0.929149006146672,-0.424691674581802));
#8624=CARTESIAN_POINT('Ctrl Pts',(-2.235,-0.934295189375141,-0.416003614975756));
#8625=CARTESIAN_POINT('Ctrl Pts',(-2.235,-0.95714587072572,-0.377425882159267));
#8626=CARTESIAN_POINT('Ctrl Pts',(-2.235,-0.977521859790832,-0.337484205077708));
#8627=CARTESIAN_POINT('Ctrl Pts',(-2.235,-0.995355662607526,-0.296493718490565));
#8628=CARTESIAN_POINT('Ctrl Pts',(-2.235,-1.01365427183518,-0.254434887638901));
#8629=CARTESIAN_POINT('Ctrl Pts',(-2.235,-1.02927729005099,-0.211271007625217));
#8630=CARTESIAN_POINT('Ctrl Pts',(-2.235,-1.0421180641197,-0.167300381368861));
#8631=CARTESIAN_POINT('Ctrl Pts',(-2.235,-1.04971059252501,-0.141301307865673));
#8632=CARTESIAN_POINT('Ctrl Pts',(-2.235,-1.05632970833611,-0.115019449284481));
#8633=CARTESIAN_POINT('Ctrl Pts',(-2.235,-1.06194617544159,-0.0885117973462398));
#8634=CARTESIAN_POINT('Ctrl Pts',(-2.235,-1.06506954309429,-0.0737706547279307));
#8635=CARTESIAN_POINT('Ctrl Pts',(-2.235,-1.067882731821,-0.0589596333448952));
#8636=CARTESIAN_POINT('Ctrl Pts',(-2.235,-1.07037988124494,-0.0440882456579739));
#8637=CARTESIAN_POINT('Ctrl Pts',(-2.235,-1.0716748055031,-0.0363765242512822));
#8638=CARTESIAN_POINT('Ctrl Pts',(-2.235,-1.07288442173141,-0.0286499953000482));
#8639=CARTESIAN_POINT('Ctrl Pts',(-2.235,-1.07400675594759,-0.0209196560664691));
#8640=CARTESIAN_POINT('Ctrl Pts',(-2.235,-1.08080241816933,0.0258870558144123));
#8641=CARTESIAN_POINT('Ctrl Pts',(-2.235,-1.08441805875872,0.0729268356242396));
#8642=CARTESIAN_POINT('Ctrl Pts',(-2.235,-1.08475384304639,0.119882946622176));
#8643=CARTESIAN_POINT('Ctrl Pts',(-2.235,-1.08483257546759,0.130892896892274));
#8644=CARTESIAN_POINT('Ctrl Pts',(-2.235,-1.08473080181681,0.141898373671195));
#8645=CARTESIAN_POINT('Ctrl Pts',(-2.235,-1.08444687417653,0.152895498319631));
#8646=CARTESIAN_POINT('Ctrl Pts',(-2.235,-1.08323508593218,0.199830648265685));
#8647=CARTESIAN_POINT('Ctrl Pts',(-2.235,-1.07871004096183,0.246612966455125));
#8648=CARTESIAN_POINT('Ctrl Pts',(-2.235,-1.07107744747181,0.293014825827104));
#8649=CARTESIAN_POINT('Ctrl Pts',(-2.235,-1.06749579235591,0.314789266877131));
#8650=CARTESIAN_POINT('Ctrl Pts',(-2.235,-1.0632289940904,0.336480057213568));
#8651=CARTESIAN_POINT('Ctrl Pts',(-2.235,-1.05829395685729,0.358063870176975));
#8652=CARTESIAN_POINT('Ctrl Pts',(-2.235,-1.05644573327181,0.366147236177911));
#8653=CARTESIAN_POINT('Ctrl Pts',(-2.235,-1.05450349182407,0.374216640931737));
#8654=CARTESIAN_POINT('Ctrl Pts',(-2.235,-1.0524688488774,0.382267600376829));
#8655=CARTESIAN_POINT('Ctrl Pts',(-2.235,-1.04090512293783,0.428024566593539));
#8656=CARTESIAN_POINT('Ctrl Pts',(-2.235,-1.02641643613206,0.472969040823713));
#8657=CARTESIAN_POINT('Ctrl Pts',(-2.235,-1.00923443573082,0.516879291823335));
#8658=CARTESIAN_POINT('Ctrl Pts',(-2.235,-0.991633669262111,0.561859739697787));
#8659=CARTESIAN_POINT('Ctrl Pts',(-2.235,-0.971206522360287,0.605755914128234));
#8660=CARTESIAN_POINT('Ctrl Pts',(-2.235,-0.948146909593293,0.648332705241361));
#8661=CARTESIAN_POINT('Ctrl Pts',(-2.235,-0.935103628555331,0.672415549033863));
#8662=CARTESIAN_POINT('Ctrl Pts',(-2.235,-0.92121713659497,0.696076245707203));
#8663=CARTESIAN_POINT('Ctrl Pts',(-2.235,-0.906515397927934,0.719270808256462));
#8664=CARTESIAN_POINT('Ctrl Pts',(-2.235,-0.895731693398996,0.736283987097004));
#8665=CARTESIAN_POINT('Ctrl Pts',(-2.235,-0.88450926307828,0.753046354789358));
#8666=CARTESIAN_POINT('Ctrl Pts',(-2.235,-0.872857527545231,0.769539831521511));
#8667=CARTESIAN_POINT('Ctrl Pts',(-2.235,-0.867086149421807,0.777709437716325));
#8668=CARTESIAN_POINT('Ctrl Pts',(-2.235,-0.861208513998563,0.785814086476887));
#8669=CARTESIAN_POINT('Ctrl Pts',(-2.235,-0.855236830129837,0.79383707455631));
#8670=CARTESIAN_POINT('Ctrl Pts',(-2.235,-0.825119235334744,0.834300218509289));
#8671=CARTESIAN_POINT('Ctrl Pts',(-2.235,-0.792554804383182,0.872772326773698));
#8672=CARTESIAN_POINT('Ctrl Pts',(-2.235,-0.7577578394247,0.909007312729686));
#8673=CARTESIAN_POINT('Ctrl Pts',(-2.235,-0.723176138298807,0.945018138849895));
#8674=CARTESIAN_POINT('Ctrl Pts',(-2.235,-0.686388893817687,0.978820512031619));
#8675=CARTESIAN_POINT('Ctrl Pts',(-2.235,-0.647559107541456,1.010155505039));
#8676=CARTESIAN_POINT('Ctrl Pts',(-2.235,-0.610523528048654,1.04004260295335));
#8677=CARTESIAN_POINT('Ctrl Pts',(-2.235,-0.571629106455326,1.06768579765986));
#8678=CARTESIAN_POINT('Ctrl Pts',(-2.235,-0.530983509300122,1.09283187766981));
#8679=CARTESIAN_POINT('Ctrl Pts',(-2.235,-0.557525174626851,-0.780836043637726));
#8680=CARTESIAN_POINT('Ctrl Pts',(-2.2143164228436,-0.331791173027909,-0.939557070115845));
#8681=CARTESIAN_POINT('Ctrl Pts',(-2.17026779978903,0.305102622594342,-1.06385016155341));
#8682=CARTESIAN_POINT('Ctrl Pts',(-2.10285413083626,1.05900093864512,-0.381087916994184));
#8683=CARTESIAN_POINT('Ctrl Pts',(-2.03275899314173,0.907151642232085,0.666313302776059));
#8684=CARTESIAN_POINT('Ctrl Pts',(-1.96266385544718,-0.0465745614418721,
1.12446411646007));
#8685=CARTESIAN_POINT('Ctrl Pts',(-1.90278663498807,-0.826057143873035,
0.66703697687178));
#8686=CARTESIAN_POINT('Ctrl Pts',(-1.86627446042713,-0.956397313027637,
0.176203929829702));
#8687=CARTESIAN_POINT('Ctrl Pts',(-1.85312733176438,-0.956897745415108,
-0.000286873987960694));
#8688=CARTESIAN_POINT('Origin',(-2.235,-1.13809670924099E-16,0.));
#8689=CARTESIAN_POINT('',(-2.235,-1.215,-1.48794586096403E-16));
#8690=CARTESIAN_POINT('Origin',(-2.235,0.,0.));
#8691=CARTESIAN_POINT('Origin',(-2.235,0.,0.));
#8692=CARTESIAN_POINT('',(-2.235,0.556433207999849,-0.780144311992978));
#8693=CARTESIAN_POINT('Ctrl Pts',(-2.235,0.532202955181986,1.09392695412892));
#8694=CARTESIAN_POINT('Ctrl Pts',(-2.235,0.570935961351045,1.07029732077084));
#8695=CARTESIAN_POINT('Ctrl Pts',(-2.235,0.608171312273549,1.04445758783552));
#8696=CARTESIAN_POINT('Ctrl Pts',(-2.235,0.643678611685364,1.0164050085206));
#8697=CARTESIAN_POINT('Ctrl Pts',(-2.235,0.680276879397345,0.987490508550553));
#8698=CARTESIAN_POINT('Ctrl Pts',(-2.235,0.715039639510439,0.956224271593212));
#8699=CARTESIAN_POINT('Ctrl Pts',(-2.235,0.747848230138463,0.922845129327136));
#8700=CARTESIAN_POINT('Ctrl Pts',(-2.235,0.758186628312356,0.912326943180031));
#8701=CARTESIAN_POINT('Ctrl Pts',(-2.235,0.768330729852818,0.901598830932486));
#8702=CARTESIAN_POINT('Ctrl Pts',(-2.235,0.778276094069858,0.890667991214823));
#8703=CARTESIAN_POINT('Ctrl Pts',(-2.235,0.785744826798305,0.882459189750435));
#8704=CARTESIAN_POINT('Ctrl Pts',(-2.235,0.793094836869084,0.874143334991178));
#8705=CARTESIAN_POINT('Ctrl Pts',(-2.235,0.800324164370073,0.865724719557378));
#8706=CARTESIAN_POINT('Ctrl Pts',(-2.235,0.832777416305257,0.827932622355924));
#8707=CARTESIAN_POINT('Ctrl Pts',(-2.235,0.862807405761098,0.788065939422894));
#8708=CARTESIAN_POINT('Ctrl Pts',(-2.235,0.890275454946883,0.746423779773389));
#8709=CARTESIAN_POINT('Ctrl Pts',(-2.235,0.907683361818825,0.720033014552966));
#8710=CARTESIAN_POINT('Ctrl Pts',(-2.235,0.924061359764043,0.692928619453533));
#8711=CARTESIAN_POINT('Ctrl Pts',(-2.235,0.939363621583103,0.665184089794141));
#8712=CARTESIAN_POINT('Ctrl Pts',(-2.235,0.945117925016288,0.654750962707512));
#8713=CARTESIAN_POINT('Ctrl Pts',(-2.235,0.95072002395897,0.644227307812222));
#8714=CARTESIAN_POINT('Ctrl Pts',(-2.235,0.956167161564349,0.633617026575594));
#8715=CARTESIAN_POINT('Ctrl Pts',(-2.235,0.960593935695727,0.624994274240761));
#8716=CARTESIAN_POINT('Ctrl Pts',(-2.235,0.964914147803501,0.616322489816617));
#8717=CARTESIAN_POINT('Ctrl Pts',(-2.235,0.969126132571279,0.607605606961102));
#8718=CARTESIAN_POINT('Ctrl Pts',(-2.235,0.990896948251949,0.562549971572965));
#8719=CARTESIAN_POINT('Ctrl Pts',(-2.235,1.00978844472556,0.516275903978842));
#8720=CARTESIAN_POINT('Ctrl Pts',(-2.235,1.02565574506571,0.469085560530428));
#8721=CARTESIAN_POINT('Ctrl Pts',(-2.235,1.04061566397402,0.424593826202019));
#8722=CARTESIAN_POINT('Ctrl Pts',(-2.235,1.05288718297695,0.379286485515974));
#8723=CARTESIAN_POINT('Ctrl Pts',(-2.235,1.06229978775484,0.333415361987417));
#8724=CARTESIAN_POINT('Ctrl Pts',(-2.235,1.06743427542606,0.308393094105121));
#8725=CARTESIAN_POINT('Ctrl Pts',(-2.235,1.07171720862766,0.283203138768487));
#8726=CARTESIAN_POINT('Ctrl Pts',(-2.235,1.07511448199102,0.257887868864709));
#8727=CARTESIAN_POINT('Ctrl Pts',(-2.235,1.07668747296967,0.246166500896409));
#8728=CARTESIAN_POINT('Ctrl Pts',(-2.235,1.07807052747635,0.234418289336243));
#8729=CARTESIAN_POINT('Ctrl Pts',(-2.235,1.07925991542886,0.222647573559399));
#8730=CARTESIAN_POINT('Ctrl Pts',(-2.235,1.08006108948689,0.214718796321534));
#8731=CARTESIAN_POINT('Ctrl Pts',(-2.235,1.08077410511126,0.206781914938808));
#8732=CARTESIAN_POINT('Ctrl Pts',(-2.235,1.08139741040059,0.198847166680972));
#8733=CARTESIAN_POINT('Ctrl Pts',(-2.235,1.08495418750844,0.153568983673532));
#8734=CARTESIAN_POINT('Ctrl Pts',(-2.235,1.08560262210768,0.108276498550504));
#8735=CARTESIAN_POINT('Ctrl Pts',(-2.235,1.08319924414589,0.0632045017416759));
#8736=CARTESIAN_POINT('Ctrl Pts',(-2.235,1.08259781979703,0.0519256281048941));
#8737=CARTESIAN_POINT('Ctrl Pts',(-2.235,1.08180503941071,0.0406606062533197));
#8738=CARTESIAN_POINT('Ctrl Pts',(-2.235,1.08081814896937,0.0294132343569632));
#8739=CARTESIAN_POINT('Ctrl Pts',(-2.235,1.07718136004208,-0.0120344439874117));
#8740=CARTESIAN_POINT('Ctrl Pts',(-2.235,1.07091080750056,-0.0532438047629177));
#8741=CARTESIAN_POINT('Ctrl Pts',(-2.235,1.06211640235717,-0.0940174914631829));
#8742=CARTESIAN_POINT('Ctrl Pts',(-2.235,1.05784493676256,-0.113821377805274));
#8743=CARTESIAN_POINT('Ctrl Pts',(-2.235,1.05297763225743,-0.133522222447208));
#8744=CARTESIAN_POINT('Ctrl Pts',(-2.235,1.04752483525318,-0.153095587959791));
#8745=CARTESIAN_POINT('Ctrl Pts',(-2.235,1.04427566217819,-0.164758822839231));
#8746=CARTESIAN_POINT('Ctrl Pts',(-2.235,1.0408185757323,-0.176376768999421));
#8747=CARTESIAN_POINT('Ctrl Pts',(-2.235,1.03715555713669,-0.187944005245821));
#8748=CARTESIAN_POINT('Ctrl Pts',(-2.235,1.03469686685762,-0.195708162203401));
#8749=CARTESIAN_POINT('Ctrl Pts',(-2.235,1.03214638620948,-0.203446123892296));
#8750=CARTESIAN_POINT('Ctrl Pts',(-2.235,1.02950774573197,-0.211148589345367));
#8751=CARTESIAN_POINT('Ctrl Pts',(-2.235,1.01489274295801,-0.253811299526025));
#8752=CARTESIAN_POINT('Ctrl Pts',(-2.235,0.997554076096989,-0.295459604389543));
#8753=CARTESIAN_POINT('Ctrl Pts',(-2.235,0.977655983421763,-0.335851464592034));
#8754=CARTESIAN_POINT('Ctrl Pts',(-2.235,0.957880950340033,-0.375993521661219));
#8755=CARTESIAN_POINT('Ctrl Pts',(-2.235,0.935577178122234,-0.414895529727038));
#8756=CARTESIAN_POINT('Ctrl Pts',(-2.235,0.910868861591031,-0.452285030065642));
#8757=CARTESIAN_POINT('Ctrl Pts',(-2.235,0.899647016373272,-0.469266323997152));
#8758=CARTESIAN_POINT('Ctrl Pts',(-2.235,0.887928751362612,-0.485935068401997));
#8759=CARTESIAN_POINT('Ctrl Pts',(-2.235,0.875723886356509,-0.502262586036078));
#8760=CARTESIAN_POINT('Ctrl Pts',(-2.235,0.868758508523048,-0.511580782455866));
#8761=CARTESIAN_POINT('Ctrl Pts',(-2.235,0.861634625064288,-0.520787800698161));
#8762=CARTESIAN_POINT('Ctrl Pts',(-2.235,0.854353937554375,-0.529877976291384));
#8763=CARTESIAN_POINT('Ctrl Pts',(-2.235,0.847884766054935,-0.537954947702741));
#8764=CARTESIAN_POINT('Ctrl Pts',(-2.235,0.841290357473231,-0.545941104261957));
#8765=CARTESIAN_POINT('Ctrl Pts',(-2.235,0.8345868346318,-0.55381546899887));
#8766=CARTESIAN_POINT('Ctrl Pts',(-2.235,0.806640848200088,-0.586642520580773));
#8767=CARTESIAN_POINT('Ctrl Pts',(-2.235,0.776747360164672,-0.617598927517484));
#8768=CARTESIAN_POINT('Ctrl Pts',(-2.235,0.745029604371381,-0.646447765737017));
#8769=CARTESIAN_POINT('Ctrl Pts',(-2.235,0.71443401474895,-0.674275939363204));
#8770=CARTESIAN_POINT('Ctrl Pts',(-2.235,0.682140147959964,-0.700143461935094));
#8771=CARTESIAN_POINT('Ctrl Pts',(-2.235,0.648238779596853,-0.723794792910752));
#8772=CARTESIAN_POINT('Ctrl Pts',(-2.235,0.618829490798728,-0.744312219100546));
#8773=CARTESIAN_POINT('Ctrl Pts',(-2.235,0.588209931826527,-0.7631614344557));
#8774=CARTESIAN_POINT('Ctrl Pts',(-2.235,0.556433207999848,-0.780144311992979));
#8775=CARTESIAN_POINT('Origin',(-2.235,0.,0.));
#8776=CARTESIAN_POINT('Origin',(-3.06687266823562,0.,0.));
#8777=CARTESIAN_POINT('Ctrl Pts',(-2.235,0.556433207999848,-0.780144311992979));
#8778=CARTESIAN_POINT('Ctrl Pts',(-2.21163495410182,0.81094560401685,-0.598614886200353));
#8779=CARTESIAN_POINT('Ctrl Pts',(-2.16490486230546,1.12483260886138,0.029436645387845));
#8780=CARTESIAN_POINT('Ctrl Pts',(-2.09480972461091,0.602343789565177,0.951528243211824));
#8781=CARTESIAN_POINT('Ctrl Pts',(-2.02471458691638,-0.45292157341433,1.02997591440566));
#8782=CARTESIAN_POINT('Ctrl Pts',(-1.97373556812461,-0.929108146284966,
0.425949523674369));
#8783=CARTESIAN_POINT('Ctrl Pts',(-1.94612159523103,-0.959171617511514,
0.0575656004424785));
#8784=CARTESIAN_POINT('Ctrl Pts',(-1.94187266823562,-0.958689328197825,
0.000800959330899747));
#8785=CARTESIAN_POINT('Ctrl Pts',(-2.38323468161444,0.70552188648037,-0.989173325407221));
#8786=CARTESIAN_POINT('Ctrl Pts',(-2.35986963571626,1.02822740295379,-0.759005569249601));
#8787=CARTESIAN_POINT('Ctrl Pts',(-2.31313954391989,1.42621614376893,0.0373237924823694));
#8788=CARTESIAN_POINT('Ctrl Pts',(-2.24304440622535,0.763733581342751,1.20647724028423));
#8789=CARTESIAN_POINT('Ctrl Pts',(-2.17294926853081,-0.574275723139484,
1.30594389355896));
#8790=CARTESIAN_POINT('Ctrl Pts',(-2.10285413083627,-1.404453333381,0.252891972003963));
#8791=CARTESIAN_POINT('Ctrl Pts',(-2.03275899314172,-0.99349569060003,-1.02455353802336));
#8792=CARTESIAN_POINT('Ctrl Pts',(-1.96266385544718,0.295607537464514,-1.39601730052373));
#8793=CARTESIAN_POINT('Ctrl Pts',(-1.89256871775264,1.3234073776496,-0.533899580371048));
#8794=CARTESIAN_POINT('Ctrl Pts',(-1.8224735800581,1.18157746100638,0.800215952773212));
#8795=CARTESIAN_POINT('Ctrl Pts',(-1.75237844236356,-0.00456266479474856,
1.42701921510532));
#8796=CARTESIAN_POINT('Ctrl Pts',(-1.68228330466901,-1.18666438626039,0.792632946367487));
#8797=CARTESIAN_POINT('Ctrl Pts',(-1.61218816697447,-1.31997416439636,-0.542314941584932));
#8798=CARTESIAN_POINT('Ctrl Pts',(-1.54209302927993,-0.286665770377846,
-1.39794551284947));
#8799=CARTESIAN_POINT('Ctrl Pts',(-1.47199789158539,1.00000206223092,-1.01805219163445));
#8800=CARTESIAN_POINT('Ctrl Pts',(-1.40190275389085,1.40285079895742,0.261616380034874));
#8801=CARTESIAN_POINT('Ctrl Pts',(-1.3318076161963,0.565834901448313,1.31006237061056));
#8802=CARTESIAN_POINT('Ctrl Pts',(-1.26171247850176,-0.771275778959115,
1.20065271063163));
#8803=CARTESIAN_POINT('Ctrl Pts',(-1.19161734080722,-1.4267193361598,0.0300846251506579));
#8804=CARTESIAN_POINT('Ctrl Pts',(-1.12152220311268,-0.821203001667309,
-1.1670727864228));
#8805=CARTESIAN_POINT('Ctrl Pts',(-1.05142706541813,0.510107032224125,-1.33275030154274));
#8806=CARTESIAN_POINT('Ctrl Pts',(-0.981331927723592,1.39057553246452,-0.320520175572548));
#8807=CARTESIAN_POINT('Ctrl Pts',(-0.911236790029049,1.04202855526106,0.974992758628685));
#8808=CARTESIAN_POINT('Ctrl Pts',(-0.841141652334507,-0.22748139059697,
1.40878711583204));
#8809=CARTESIAN_POINT('Ctrl Pts',(-0.771046514639965,-1.29593988473495,
0.597475610961073));
#8810=CARTESIAN_POINT('Ctrl Pts',(-0.700951376945422,-1.21902254189685,
-0.741905247072227));
#8811=CARTESIAN_POINT('Ctrl Pts',(-0.63085623925088,-0.0647137586129758,
-1.42555841256541));
#8812=CARTESIAN_POINT('Ctrl Pts',(-0.560761101556339,1.14679453675556,-0.84931334494321));
#8813=CARTESIAN_POINT('Ctrl Pts',(-0.490665963861794,1.34473723177141,0.477637547336413));
#8814=CARTESIAN_POINT('Ctrl Pts',(-0.420570826167255,0.354193056453061,
1.38231523117118));
#8815=CARTESIAN_POINT('Ctrl Pts',(-0.35047568847271,-0.949423132758245,
1.06552304268868));
#8816=CARTESIAN_POINT('Ctrl Pts',(-0.280380550778169,-1.4138654371531,-0.193463280166926));
#8817=CARTESIAN_POINT('Ctrl Pts',(-0.210285413083626,-0.628816545074822,
-1.28057479748412));
#8818=CARTESIAN_POINT('Ctrl Pts',(-0.140190275389084,0.71219637134211,-1.23759954882087));
#8819=CARTESIAN_POINT('Ctrl Pts',(-0.0700951376945416,1.42337502914537,
-0.097411912196576));
#8820=CARTESIAN_POINT('Ctrl Pts',(-0.0233650458981805,1.05930884981436,
0.714986578225072));
#8821=CARTESIAN_POINT('Ctrl Pts',(0.,0.746592769117024,0.958553199933198));
#8822=CARTESIAN_POINT('Ctrl Pts',(-2.33382312107629,0.655825660320196,-0.919496987602474));
#8823=CARTESIAN_POINT('Ctrl Pts',(-2.31045807517811,0.955800136641479,-0.705542008233185));
#8824=CARTESIAN_POINT('Ctrl Pts',(-2.26372798338175,1.32575496546642,0.0346947434508616));
#8825=CARTESIAN_POINT('Ctrl Pts',(-2.19363284568721,0.709936984083557,1.1214942412601));
#8826=CARTESIAN_POINT('Ctrl Pts',(-2.12353770799267,-0.533824339897765,
1.21395456717453));
#8827=CARTESIAN_POINT('Ctrl Pts',(-2.05344257029812,-1.30552510475396,0.235078525141954));
#8828=CARTESIAN_POINT('Ctrl Pts',(-1.98334743260358,-0.923514889897269,
-0.952385054926656));
#8829=CARTESIAN_POINT('Ctrl Pts',(-1.91325229490904,0.274785250703467,-1.29768329725639));
#8830=CARTESIAN_POINT('Ctrl Pts',(-1.8431571572145,1.23018794165192,-0.49629225053284));
#8831=CARTESIAN_POINT('Ctrl Pts',(-1.77306201951995,1.09834837647596,0.743849575304207));
#8832=CARTESIAN_POINT('Ctrl Pts',(-1.70296688182541,-0.00424127544329419,
1.32650146929509));
#8833=CARTESIAN_POINT('Ctrl Pts',(-1.63287174413087,-1.10307698401832,0.736800707964236));
#8834=CARTESIAN_POINT('Ctrl Pts',(-1.56277660643633,-1.22699656036104,-0.504114842476036));
#8835=CARTESIAN_POINT('Ctrl Pts',(-1.49268146874178,-0.266473332368378,
-1.29947568831611));
#8836=CARTESIAN_POINT('Ctrl Pts',(-1.42258633104725,0.929562959493534,-0.946341656599571));
#8837=CARTESIAN_POINT('Ctrl Pts',(-1.3524911933527,1.3040354511845,0.243188394966574));
#8838=CARTESIAN_POINT('Ctrl Pts',(-1.28239605565816,0.525978080886761,1.21778294299622));
#8839=CARTESIAN_POINT('Ctrl Pts',(-1.21230091796361,-0.716947917162748,
1.11607998540401));
#8840=CARTESIAN_POINT('Ctrl Pts',(-1.14220578026907,-1.32622271350986,0.027965495518989));
#8841=CARTESIAN_POINT('Ctrl Pts',(-1.07211064257453,-0.763358318353705,
-1.08486539604858));
#8842=CARTESIAN_POINT('Ctrl Pts',(-1.00201550487999,0.474175624673083,-1.23887275972625));
#8843=CARTESIAN_POINT('Ctrl Pts',(-0.931920367185447,1.29262484166609,-0.297943068555193));
#8844=CARTESIAN_POINT('Ctrl Pts',(-0.861825229490902,0.96862915016825,0.906315285164235));
#8845=CARTESIAN_POINT('Ctrl Pts',(-0.791730091796362,-0.211457838598131,
1.30955362008722));
#8846=CARTESIAN_POINT('Ctrl Pts',(-0.721634954101819,-1.20465523030266,
0.555390051807641));
#8847=CARTESIAN_POINT('Ctrl Pts',(-0.651539816407277,-1.1331558649059,-0.689646214922488));
#8848=CARTESIAN_POINT('Ctrl Pts',(-0.581444678712735,-0.0601553889219246,
-1.32514356416317));
#8849=CARTESIAN_POINT('Ctrl Pts',(-0.511349541018193,1.06601552514733,-0.789488598354958));
#8850=CARTESIAN_POINT('Ctrl Pts',(-0.44125440332365,1.25001534308628,0.443993256450644));
#8851=CARTESIAN_POINT('Ctrl Pts',(-0.371159265629109,0.329244066811271,
1.28494638738429));
#8852=CARTESIAN_POINT('Ctrl Pts',(-0.301064127934565,-0.882546757083162,
0.990468710395036));
#8853=CARTESIAN_POINT('Ctrl Pts',(-0.230968990240023,-1.31427422974869,
-0.179835928402081));
#8854=CARTESIAN_POINT('Ctrl Pts',(-0.160873852545481,-0.584523363196095,
-1.1903724437793));
#8855=CARTESIAN_POINT('Ctrl Pts',(-0.0907787148509382,0.662030001426586,
-1.15042432682916));
#8856=CARTESIAN_POINT('Ctrl Pts',(-0.0206835771563963,1.32311397599501,
-0.0905503186557062));
#8857=CARTESIAN_POINT('Ctrl Pts',(0.026046514639965,0.984692238788337,0.664623669045569));
#8858=CARTESIAN_POINT('Ctrl Pts',(0.0494115605381455,0.694003552801305,
0.891033711844625));
#8859=CARTESIAN_POINT('Ctrl Pts',(-2.28441156053815,0.606129434160022,-0.849820649797726));
#8860=CARTESIAN_POINT('Ctrl Pts',(-2.26104651463996,0.883372870329165,-0.652078447216769));
#8861=CARTESIAN_POINT('Ctrl Pts',(-2.2143164228436,1.2252937871639,0.0320656944193542));
#8862=CARTESIAN_POINT('Ctrl Pts',(-2.14422128514906,0.656140386824367,1.03651124223596));
#8863=CARTESIAN_POINT('Ctrl Pts',(-2.07412614745452,-0.493372956656047,
1.1219652407901));
#8864=CARTESIAN_POINT('Ctrl Pts',(-2.00403100975998,-1.20659687612692,0.217265078279945));
#8865=CARTESIAN_POINT('Ctrl Pts',(-1.93393587206544,-0.85353408919451,-0.880216571829947));
#8866=CARTESIAN_POINT('Ctrl Pts',(-1.86384073437089,0.253962963942421,-1.19934929398904));
#8867=CARTESIAN_POINT('Ctrl Pts',(-1.79374559667635,1.13696850565425,-0.458684920694631));
#8868=CARTESIAN_POINT('Ctrl Pts',(-1.72365045898181,1.01511929194553,0.687483197835202));
#8869=CARTESIAN_POINT('Ctrl Pts',(-1.65355532128727,-0.00391988609183947,
1.22598372348486));
#8870=CARTESIAN_POINT('Ctrl Pts',(-1.58346018359272,-1.01948958177625,0.680968469560984));
#8871=CARTESIAN_POINT('Ctrl Pts',(-1.51336504589818,-1.13401895632571,-0.465914743367139));
#8872=CARTESIAN_POINT('Ctrl Pts',(-1.44326990820364,-0.246280894358909,
-1.20100586378275));
#8873=CARTESIAN_POINT('Ctrl Pts',(-1.37317477050909,0.859123856756142,-0.874631121564689));
#8874=CARTESIAN_POINT('Ctrl Pts',(-1.30307963281455,1.20522010341157,0.224760409898275));
#8875=CARTESIAN_POINT('Ctrl Pts',(-1.23298449512001,0.48612126032521,1.12550351538188));
#8876=CARTESIAN_POINT('Ctrl Pts',(-1.16288935742547,-0.662620055366384,
1.0315072601764));
#8877=CARTESIAN_POINT('Ctrl Pts',(-1.09279421973093,-1.22572609085992,0.0258463658873193));
#8878=CARTESIAN_POINT('Ctrl Pts',(-1.02269908203638,-0.705513635040103,
-1.00265800567435));
#8879=CARTESIAN_POINT('Ctrl Pts',(-0.952603944341843,0.438244217122043,
-1.14499521790977));
#8880=CARTESIAN_POINT('Ctrl Pts',(-0.8825088066473,1.19467415086766,-0.275365961537841));
#8881=CARTESIAN_POINT('Ctrl Pts',(-0.812413668952758,0.895229745075445,
0.837637811699788));
#8882=CARTESIAN_POINT('Ctrl Pts',(-0.742318531258216,-0.195434286599291,
1.2103201243424));
#8883=CARTESIAN_POINT('Ctrl Pts',(-0.672223393563674,-1.11337057587037,
0.51330449265421));
#8884=CARTESIAN_POINT('Ctrl Pts',(-0.602128255869132,-1.04728918791495,
-0.637387182772751));
#8885=CARTESIAN_POINT('Ctrl Pts',(-0.53203311817459,-0.0555970192308733,
-1.22472871576093));
#8886=CARTESIAN_POINT('Ctrl Pts',(-0.461937980480047,0.985236513539103,
-0.72966385176671));
#8887=CARTESIAN_POINT('Ctrl Pts',(-0.391842842785505,1.15529345440114,0.410348965564877));
#8888=CARTESIAN_POINT('Ctrl Pts',(-0.321747705090963,0.304295077169481,
1.18757754359741));
#8889=CARTESIAN_POINT('Ctrl Pts',(-0.25165256739642,-0.815670381408078,
0.915414378101397));
#8890=CARTESIAN_POINT('Ctrl Pts',(-0.181557429701878,-1.21468302234429,
-0.166208576637237));
#8891=CARTESIAN_POINT('Ctrl Pts',(-0.111462292007335,-0.540230181317368,
-1.10017009007449));
#8892=CARTESIAN_POINT('Ctrl Pts',(-0.0413671543127928,0.611863631511061,
-1.06324910483746));
#8893=CARTESIAN_POINT('Ctrl Pts',(0.0287279833817493,1.22285292284465,-0.0836887251148355));
#8894=CARTESIAN_POINT('Ctrl Pts',(0.0754580751781104,0.910075627762319,
0.614260759866067));
#8895=CARTESIAN_POINT('Ctrl Pts',(0.0988231210762909,0.641414336485586,
0.823514223756052));
#8896=CARTESIAN_POINT('Ctrl Pts',(-2.235,0.556433207999848,-0.780144311992979));
#8897=CARTESIAN_POINT('Ctrl Pts',(-2.21163495410182,0.81094560401685,-0.598614886200353));
#8898=CARTESIAN_POINT('Ctrl Pts',(-2.16490486230546,1.12483260886138,0.029436645387845));
#8899=CARTESIAN_POINT('Ctrl Pts',(-2.09480972461091,0.602343789565177,0.951528243211824));
#8900=CARTESIAN_POINT('Ctrl Pts',(-2.02471458691638,-0.45292157341433,1.02997591440566));
#8901=CARTESIAN_POINT('Ctrl Pts',(-1.95461944922183,-1.10766864749988,0.199451631417939));
#8902=CARTESIAN_POINT('Ctrl Pts',(-1.88452431152729,-0.78355328849175,-0.808048088733242));
#8903=CARTESIAN_POINT('Ctrl Pts',(-1.81442917383274,0.233140677181374,-1.1010152907217));
#8904=CARTESIAN_POINT('Ctrl Pts',(-1.74433403613821,1.04374906965657,-0.421077590856424));
#8905=CARTESIAN_POINT('Ctrl Pts',(-1.67423889844366,0.931890207415111,0.631116820366198));
#8906=CARTESIAN_POINT('Ctrl Pts',(-1.60414376074912,-0.00359849674038535,
1.12546597767462));
#8907=CARTESIAN_POINT('Ctrl Pts',(-1.53404862305458,-0.935902179534174,
0.625136231157733));
#8908=CARTESIAN_POINT('Ctrl Pts',(-1.46395348536004,-1.04104135229038,-0.427714644258242));
#8909=CARTESIAN_POINT('Ctrl Pts',(-1.39385834766549,-0.226088456349441,
-1.10253603924939));
#8910=CARTESIAN_POINT('Ctrl Pts',(-1.32376320997095,0.788684754018751,-0.802920586529807));
#8911=CARTESIAN_POINT('Ctrl Pts',(-1.25366807227641,1.10640475563864,0.206332424829975));
#8912=CARTESIAN_POINT('Ctrl Pts',(-1.18357293458187,0.446264439763658,1.03322408776754));
#8913=CARTESIAN_POINT('Ctrl Pts',(-1.11347779688732,-0.608292193570018,
0.946934534948777));
#8914=CARTESIAN_POINT('Ctrl Pts',(-1.04338265919278,-1.12522946820998,0.0237272362556514));
#8915=CARTESIAN_POINT('Ctrl Pts',(-0.973287521498239,-0.6476689517265,-0.920450615300125));
#8916=CARTESIAN_POINT('Ctrl Pts',(-0.903192383803697,0.402312809571003,
-1.05111767609328));
#8917=CARTESIAN_POINT('Ctrl Pts',(-0.833097246109155,1.09672346006924,-0.252788854520488));
#8918=CARTESIAN_POINT('Ctrl Pts',(-0.763002108414613,0.821830339982639,
0.76896033823534));
#8919=CARTESIAN_POINT('Ctrl Pts',(-0.69290697072007,-0.17941073460045,1.11108662859757));
#8920=CARTESIAN_POINT('Ctrl Pts',(-0.622811833025529,-1.02208592143808,
0.47121893350078));
#8921=CARTESIAN_POINT('Ctrl Pts',(-0.552716695330986,-0.961422510923996,
-0.585128150623014));
#8922=CARTESIAN_POINT('Ctrl Pts',(-0.482621557636444,-0.0510386495398221,
-1.12431386735868));
#8923=CARTESIAN_POINT('Ctrl Pts',(-0.412526419941902,0.904457501930876,
-0.669839105178461));
#8924=CARTESIAN_POINT('Ctrl Pts',(-0.342431282247359,1.06057156571601,0.37670467467911));
#8925=CARTESIAN_POINT('Ctrl Pts',(-0.272336144552818,0.279346087527691,
1.09020869981052));
#8926=CARTESIAN_POINT('Ctrl Pts',(-0.202241006858274,-0.748794005732996,
0.840360045807757));
#8927=CARTESIAN_POINT('Ctrl Pts',(-0.132145869163732,-1.11509181493988,
-0.152581224872393));
#8928=CARTESIAN_POINT('Ctrl Pts',(-0.0620507314691897,-0.49593699943864,
-1.00996773636968));
#8929=CARTESIAN_POINT('Ctrl Pts',(0.00804440622535258,0.561697261595537,
-0.976073882845758));
#8930=CARTESIAN_POINT('Ctrl Pts',(0.0781395439198948,1.12259186969428,-0.0768271315739657));
#8931=CARTESIAN_POINT('Ctrl Pts',(0.124869635716256,0.835459016736301,0.563897850686564));
#8932=CARTESIAN_POINT('Ctrl Pts',(0.148234681614436,0.588825120169867,0.755994735667479));
#8933=CARTESIAN_POINT('',(0.,0.746592769117024,0.958553199933198));
#8934=CARTESIAN_POINT('Ctrl Pts',(0.,0.382997178453079,-0.879688698994096));
#8935=CARTESIAN_POINT('Ctrl Pts',(-9.804104464095E-17,0.4180497090205,-0.869827137061451));
#8936=CARTESIAN_POINT('Ctrl Pts',(2.83567237026956E-16,0.452404690302672,
-0.85791012243036));
#8937=CARTESIAN_POINT('Ctrl Pts',(8.60422844084496E-16,0.485870814430818,
-0.843943792735025));
#8938=CARTESIAN_POINT('Ctrl Pts',(1.54716742777456E-15,0.525712118217974,
-0.827316926054773));
#8939=CARTESIAN_POINT('Ctrl Pts',(2.72305014732216E-15,0.56429503081299,
-0.807787628815318));
#8940=CARTESIAN_POINT('Ctrl Pts',(3.27515792264421E-15,0.601481112419859,
-0.785640792695669));
#8941=CARTESIAN_POINT('Ctrl Pts',(3.45547965866087E-15,0.613626311402242,
-0.77840750217727));
#8942=CARTESIAN_POINT('Ctrl Pts',(1.97546578491965E-15,0.625626535869127,
-0.770891537608958));
#8943=CARTESIAN_POINT('Ctrl Pts',(1.99840144432528E-15,0.637451076083524,
-0.76311912782532));
#8944=CARTESIAN_POINT('Ctrl Pts',(2.068511555245E-15,0.673596530257937,
-0.73936029436834));
#8945=CARTESIAN_POINT('Ctrl Pts',(2.62962033288778E-15,0.708143337648631,
-0.713186494829503));
#8946=CARTESIAN_POINT('Ctrl Pts',(2.58126853225349E-15,0.740960712846234,
-0.684884151557313));
#8947=CARTESIAN_POINT('Ctrl Pts',(2.54780568648073E-15,0.763672643953208,
-0.665296940005706));
#8948=CARTESIAN_POINT('Ctrl Pts',(2.36504271574013E-15,0.785556143128117,
-0.644689014679008));
#8949=CARTESIAN_POINT('Ctrl Pts',(2.16493489801906E-15,0.806563371679136,
-0.623141582851505));
#8950=CARTESIAN_POINT('Ctrl Pts',(2.09787202592262E-15,0.813603601778398,
-0.615920312432832));
#8951=CARTESIAN_POINT('Ctrl Pts',(2.43023859382518E-15,0.820546530101037,
-0.608592177634928));
#8952=CARTESIAN_POINT('Ctrl Pts',(2.45636844198316E-15,0.827386584885893,
-0.601163949164734));
#8953=CARTESIAN_POINT('Ctrl Pts',(2.57239349865007E-15,0.857758661264587,
-0.568180189596812));
#8954=CARTESIAN_POINT('Ctrl Pts',(2.64260608659013E-15,0.885993699958357,
-0.533347772836182));
#8955=CARTESIAN_POINT('Ctrl Pts',(2.45636844198316E-15,0.91196016345517,
-0.496960911841512));
#8956=CARTESIAN_POINT('Ctrl Pts',(2.26527696128891E-15,0.938603380343306,
-0.459625714867984));
#8957=CARTESIAN_POINT('Ctrl Pts',(2.23712577659718E-15,0.96285922821364,
-0.420653328397313));
#8958=CARTESIAN_POINT('Ctrl Pts',(2.27595720048157E-15,0.98456136594598,
-0.3803133590392));
#8959=CARTESIAN_POINT('Ctrl Pts',(2.29891753903009E-15,0.997393458610018,
-0.356461044062117));
#8960=CARTESIAN_POINT('Ctrl Pts',(2.5501319721175E-15,1.00933220658872,
-0.332129738518424));
#8961=CARTESIAN_POINT('Ctrl Pts',(2.5951463200613E-15,1.02033716389955,
-0.307369109439727));
#8962=CARTESIAN_POINT('Ctrl Pts',(2.62017925710253E-15,1.026457132667,-0.293599471598876));
#8963=CARTESIAN_POINT('Ctrl Pts',(2.04833619180827E-15,1.03228822883295,
-0.279696991010135));
#8964=CARTESIAN_POINT('Ctrl Pts',(2.09554595897998E-15,1.03782274236849,
-0.26566975374606));
#8965=CARTESIAN_POINT('Ctrl Pts',(2.12002711331586E-15,1.04069272644498,
-0.258395772514194));
#8966=CARTESIAN_POINT('Ctrl Pts',(1.99819100377786E-15,1.04348234508209,
-0.251089570609367));
#8967=CARTESIAN_POINT('Ctrl Pts',(2.02615701994091E-15,1.04618738106416,
-0.243761494361897));
#8968=CARTESIAN_POINT('Ctrl Pts',(2.19548911505624E-15,1.06256616764341,
-0.19939055153921));
#8969=CARTESIAN_POINT('Ctrl Pts',(1.98314379665189E-15,1.0758828874101,
-0.15413046122802));
#8970=CARTESIAN_POINT('Ctrl Pts',(1.95676808090184E-15,1.08597403613616,
-0.108270278580235));
#8971=CARTESIAN_POINT('Ctrl Pts',(1.95058373071767E-15,1.08834012159423,
-0.0975173787654368));
#8972=CARTESIAN_POINT('Ctrl Pts',(2.10123556114942E-15,1.09052871862687,
-0.0867313252073607));
#8973=CARTESIAN_POINT('Ctrl Pts',(2.09554595897998E-15,1.09253740899759,
-0.0759155690421767));
#8974=CARTESIAN_POINT('Ctrl Pts',(2.07179073811209E-15,1.10111046158471,
-0.0297541258821798));
#8975=CARTESIAN_POINT('Ctrl Pts',(1.30472882156592E-15,1.10641089348326,
0.0169467036787));
#8976=CARTESIAN_POINT('Ctrl Pts',(1.22818422099158E-15,1.10859258913964,
0.063921494218668));
#8977=CARTESIAN_POINT('Ctrl Pts',(1.19226506616542E-15,1.10961636695646,
0.0859647835123772));
#8978=CARTESIAN_POINT('Ctrl Pts',(2.11933526040146E-15,1.10995258343241,
0.108068701556671));
#8979=CARTESIAN_POINT('Ctrl Pts',(2.1163626406917E-15,1.10961292324264,
0.130206916536899));
#8980=CARTESIAN_POINT('Ctrl Pts',(2.11524936280964E-15,1.10948571686793,
0.138497914879223));
#8981=CARTESIAN_POINT('Ctrl Pts',(1.62000664896157E-15,1.10926364458773,
0.14679480473991));
#8982=CARTESIAN_POINT('Ctrl Pts',(1.65145674912992E-15,1.10894735514218,
0.155092863980238));
#8983=CARTESIAN_POINT('Ctrl Pts',(1.83020083750486E-15,1.10714974978308,
0.202254209294043));
#8984=CARTESIAN_POINT('Ctrl Pts',(2.16858310538254E-15,1.10232217765626,
0.249228958863479));
#8985=CARTESIAN_POINT('Ctrl Pts',(2.07472927726826E-15,1.09464512145237,
0.295752061004661));
#8986=CARTESIAN_POINT('Ctrl Pts',(1.97858800625884E-15,1.08678095697574,
0.343409042728499));
#8987=CARTESIAN_POINT('Ctrl Pts',(1.28761435872327E-15,1.07592674328964,
0.390593086867689));
#8988=CARTESIAN_POINT('Ctrl Pts',(1.49880108324396E-15,1.06222327329097,
0.437033900468828));
#8989=CARTESIAN_POINT('Ctrl Pts',(1.61825517673179E-15,1.05447214409454,
0.463302338042979));
#8990=CARTESIAN_POINT('Ctrl Pts',(1.02429453254145E-15,1.0458084623023,
0.489333167506977));
#8991=CARTESIAN_POINT('Ctrl Pts',(1.02001740387436E-15,1.0362504352041,
0.515077548476332));
#8992=CARTESIAN_POINT('Ctrl Pts',(1.01688012972392E-15,1.02923962171721,
0.533961053561356));
#8993=CARTESIAN_POINT('Ctrl Pts',(2.54700031510392E-17,1.02174752170026,
0.552690444009813));
#8994=CARTESIAN_POINT('Ctrl Pts',(-3.12250225675825E-17,1.013779590733,
0.571246076127072));
#8995=CARTESIAN_POINT('Ctrl Pts',(-5.93072175778668E-17,1.00983291307628,
0.58043705669461));
#8996=CARTESIAN_POINT('Ctrl Pts',(1.75936158409219E-15,1.00576879585552,
0.589586591730184));
#8997=CARTESIAN_POINT('Ctrl Pts',(1.72084568816899E-15,1.00159570819879,
0.598675804818873));
#8998=CARTESIAN_POINT('Ctrl Pts',(1.52659355619868E-15,0.980549042795107,
0.644516592838733));
#8999=CARTESIAN_POINT('Ctrl Pts',(4.67366350146491E-16,0.956695047628213,
0.688918576168094));
#9000=CARTESIAN_POINT('Ctrl Pts',(4.71844785465692E-16,0.930192175349853,
0.731596486069531));
#9001=CARTESIAN_POINT('Ctrl Pts',(4.76295512086431E-16,0.903853280006282,
0.774010341842218));
#9002=CARTESIAN_POINT('Ctrl Pts',(7.39197774204125E-16,0.874897873665825,
0.814722558425196));
#9003=CARTESIAN_POINT('Ctrl Pts',(8.03176969377262E-16,0.843431559477603,
0.853445973895038));
#9004=CARTESIAN_POINT('Ctrl Pts',(8.64199954607425E-16,0.813419171532439,
0.890380142946133));
#9005=CARTESIAN_POINT('Ctrl Pts',(5.51860040342344E-17,0.781122019338172,
0.925505907275885));
#9006=CARTESIAN_POINT('Ctrl Pts',(0.,0.746592769117024,0.958553199933198));
#9007=CARTESIAN_POINT('Ctrl Pts',(0.,0.746592769117024,0.958553199933198));
#9008=CARTESIAN_POINT('Ctrl Pts',(-0.0233650458981805,1.05930884981436,
0.714986578225072));
#9009=CARTESIAN_POINT('Ctrl Pts',(-0.0467300917963609,1.24134193947986,
0.308787333014251));
#9010=CARTESIAN_POINT('Ctrl Pts',(-0.0700951376945414,1.21382870801208,
-0.0843435623618732));
#9011=CARTESIAN_POINT('Ctrl Pts',(-0.0934601835927222,1.18631547654429,
-0.477474457738003));
#9012=CARTESIAN_POINT('Ctrl Pts',(-0.116825229490903,0.949255923943199,
-0.857537003279436));
#9013=CARTESIAN_POINT('Ctrl Pts',(-0.140190275389084,0.607223994906499,
-1.05473081749403));
#9014=CARTESIAN_POINT('Ctrl Pts',(-0.163555321287265,0.265192065869799,
-1.25192463170862));
#9015=CARTESIAN_POINT('Ctrl Pts',(-0.186920367185445,-0.181812239602512,
-1.26624971459637));
#9016=CARTESIAN_POINT('Ctrl Pts',(-0.210285413083626,-0.536155874351713,
-1.09222700315404));
#9017=CARTESIAN_POINT('Ctrl Pts',(-0.233650458981807,-0.890499509100915,
-0.91820429171172));
#9018=CARTESIAN_POINT('Ctrl Pts',(-0.257015504879988,-1.15218247312701,
-0.555833785939323));
#9019=CARTESIAN_POINT('Ctrl Pts',(-0.280380550778169,-1.20561690440758,
-0.164817479243857));
#9020=CARTESIAN_POINT('Ctrl Pts',(-0.283622817135466,-1.21303176931378,
-0.110557837645978));
#9021=CARTESIAN_POINT('Ctrl Pts',(-0.286865083492763,-1.21643661870328,
-0.0557465950131454));
#9022=CARTESIAN_POINT('Ctrl Pts',(-0.29010734985006,-1.21601418463372,-0.00087989446188777));
#9023=CARTESIAN_POINT('Origin',(0.,1.9,3.));
#9024=CARTESIAN_POINT('',(0.,1.9,-1.2051970793194));
#9025=CARTESIAN_POINT('',(1.,1.9,-1.2051970793194));
#9026=CARTESIAN_POINT('',(0.5,1.9,-1.2051970793194));
#9027=CARTESIAN_POINT('',(0.,1.9,1.2051970793194));
#9028=CARTESIAN_POINT('',(0.,1.9,1.5));
#9029=CARTESIAN_POINT('',(1.,1.9,1.2051970793194));
#9030=CARTESIAN_POINT('',(0.5,1.9,1.2051970793194));
#9031=CARTESIAN_POINT('',(1.,1.9,1.5));
#9032=CARTESIAN_POINT('Origin',(0.,-1.9,-3.));
#9033=CARTESIAN_POINT('',(0.,-1.9,1.2051970793194));
#9034=CARTESIAN_POINT('',(1.,-1.9,1.2051970793194));
#9035=CARTESIAN_POINT('',(0.5,-1.9,1.2051970793194));
#9036=CARTESIAN_POINT('',(0.,-1.9,-1.2051970793194));
#9037=CARTESIAN_POINT('',(0.,-1.9,-1.5));
#9038=CARTESIAN_POINT('',(1.,-1.9,-1.2051970793194));
#9039=CARTESIAN_POINT('',(0.5,-1.9,-1.2051970793194));
#9040=CARTESIAN_POINT('',(1.,-1.9,-1.5));
#9041=CARTESIAN_POINT('Origin',(1.,1.5,0.));
#9042=CARTESIAN_POINT('Origin',(1.,0.,0.));
#9043=CARTESIAN_POINT('Origin',(1.,0.,0.));
#9044=CARTESIAN_POINT('',(1.,-1.5,-1.83697019872103E-16));
#9045=CARTESIAN_POINT('Origin',(1.,0.,0.));
#9046=CARTESIAN_POINT('Origin',(0.5,0.,0.));
#9047=CARTESIAN_POINT('Origin',(0.,0.,0.));
#9048=CARTESIAN_POINT('Origin',(7.15,-1.38777878078145E-16,-0.866025403784439));
#9049=CARTESIAN_POINT('',(7.01007662722764,-1.59086285808736E-16,-0.866025403784439));
#9050=CARTESIAN_POINT('',(7.01007662722764,-0.75,-0.433012701892219));
#9051=CARTESIAN_POINT('Origin',(4.4,-0.375,-0.649519052838329));
#9052=CARTESIAN_POINT('',(5.75,-1.38777878078145E-16,-0.866025403784439));
#9053=CARTESIAN_POINT('',(7.15,-1.59086285808736E-16,-0.866025403784439));
#9054=CARTESIAN_POINT('',(5.75,-0.75,-0.433012701892219));
#9055=CARTESIAN_POINT('',(5.75,-0.75,-0.433012701892219));
#9056=CARTESIAN_POINT('',(7.15,-0.75,-0.433012701892219));
#9057=CARTESIAN_POINT('Origin',(7.15,-0.75,-0.433012701892219));
#9058=CARTESIAN_POINT('',(7.01007662722764,-0.75,0.433012701892219));
#9059=CARTESIAN_POINT('Origin',(4.4,-0.75,-1.20185167898973E-16));
#9060=CARTESIAN_POINT('',(5.75,-0.75,0.433012701892219));
#9061=CARTESIAN_POINT('',(5.75,-0.75,0.433012701892219));
#9062=CARTESIAN_POINT('',(7.15,-0.75,0.433012701892219));
#9063=CARTESIAN_POINT('Origin',(7.15,-0.75,0.433012701892219));
#9064=CARTESIAN_POINT('',(7.01007662722764,5.30287619362454E-17,0.866025403784439));
#9065=CARTESIAN_POINT('Origin',(4.4,-0.375,0.649519052838329));
#9066=CARTESIAN_POINT('',(5.75,0.,0.866025403784439));
#9067=CARTESIAN_POINT('',(5.75,5.30287619362453E-17,0.866025403784439));
#9068=CARTESIAN_POINT('',(7.15,5.30287619362453E-17,0.866025403784439));
#9069=CARTESIAN_POINT('Origin',(7.15,0.,0.866025403784439));
#9070=CARTESIAN_POINT('',(7.01007662722764,0.75,0.433012701892219));
#9071=CARTESIAN_POINT('Origin',(4.4,0.375,0.649519052838329));
#9072=CARTESIAN_POINT('',(5.75,0.75,0.433012701892219));
#9073=CARTESIAN_POINT('',(5.75,0.75,0.433012701892219));
#9074=CARTESIAN_POINT('',(7.15,0.75,0.433012701892219));
#9075=CARTESIAN_POINT('Origin',(7.15,0.75,-0.43301270189222));
#9076=CARTESIAN_POINT('',(7.01007662722764,0.75,-0.43301270189222));
#9077=CARTESIAN_POINT('Origin',(4.4,0.375,-0.649519052838329));
#9078=CARTESIAN_POINT('',(5.75,0.75,-0.43301270189222));
#9079=CARTESIAN_POINT('',(7.15,0.75,-0.43301270189222));
#9080=CARTESIAN_POINT('',(5.75,-1.59086285808736E-16,-0.866025403784439));
#9081=CARTESIAN_POINT('Origin',(7.15,0.75,0.433012701892219));
#9082=CARTESIAN_POINT('Origin',(4.4,0.75,-2.40370335797945E-16));
#9083=CARTESIAN_POINT('',(5.75,0.75,-0.43301270189222));
#9084=CARTESIAN_POINT('Origin',(5.75,0.,0.));
#9085=CARTESIAN_POINT('Origin',(4.4,-2.77555756156289E-16,0.));
#9086=CARTESIAN_POINT('',(2.09511388567678,-1.5,1.83697019872103E-16));
#9087=CARTESIAN_POINT('',(2.09511388567678,-5.59822896386801E-16,1.5));
#9088=CARTESIAN_POINT('Origin',(2.09511388567678,0.,0.));
#9089=CARTESIAN_POINT('',(2.09511388567678,-5.59822896386801E-16,-1.5));
#9090=CARTESIAN_POINT('Origin',(2.09511388567678,0.,0.));
#9091=CARTESIAN_POINT('',(4.4,-2.77555756156289E-16,-2.75));
#9092=CARTESIAN_POINT('Origin',(4.4,-2.77555756156289E-16,0.));
#9093=CARTESIAN_POINT('Origin',(2.09511388567678,0.,0.));
#9094=CARTESIAN_POINT('',(4.4,-2.77555756156289E-16,2.75));
#9095=CARTESIAN_POINT('Origin',(4.4,-2.77555756156289E-16,0.));
#9096=CARTESIAN_POINT('Origin',(-2.4,1.05,0.));
#9097=CARTESIAN_POINT('',(-2.4,-1.05,-1.28587913910472E-16));
#9098=CARTESIAN_POINT('Origin',(-2.4,0.,0.));
#9099=CARTESIAN_POINT('Origin',(-2.3,0.,0.));
#9100=CARTESIAN_POINT('',(-2.3,-1.15,-1.40834381901946E-16));
#9101=CARTESIAN_POINT('Origin',(-1.1,0.,0.));
#9102=CARTESIAN_POINT('Origin',(0.,0.,0.));
#9103=CARTESIAN_POINT('Origin',(0.,2.25,0.));
#9104=CARTESIAN_POINT('Origin',(0.,0.,0.));
#9105=CARTESIAN_POINT('Origin',(0.5,0.,0.));
#9106=CARTESIAN_POINT('Origin',(1.74755694283839,0.,0.));
#9107=CARTESIAN_POINT('',(1.74755694283839,-1.5,-1.83697019872103E-16));
#11410=UNCERTAINTY_MEASURE_WITH_UNIT(LENGTH_MEASURE(0.01),#11431,
'DISTANCE_ACCURACY_VALUE',
'Maximum model space distance between geometric entities at asserted c
onnectivities');
#11416=UNCERTAINTY_MEASURE_WITH_UNIT(LENGTH_MEASURE(0.01),#11431,
'DISTANCE_ACCURACY_VALUE',
'Maximum model space distance between geometric entities at asserted c
onnectivities');
#11424=(
GEOMETRIC_REPRESENTATION_CONTEXT(3)
GLOBAL_UNCERTAINTY_ASSIGNED_CONTEXT((#11410))
GLOBAL_UNIT_ASSIGNED_CONTEXT((#11431,#11433,#11434))
REPRESENTATION_CONTEXT('','3D')
);
#11430=(
GEOMETRIC_REPRESENTATION_CONTEXT(3)
GLOBAL_UNCERTAINTY_ASSIGNED_CONTEXT((#11416))
GLOBAL_UNIT_ASSIGNED_CONTEXT((#11431,#11433,#11434))
REPRESENTATION_CONTEXT('','3D')
);
#11431=(
LENGTH_UNIT()
NAMED_UNIT(*)
SI_UNIT(.MILLI.,.METRE.)
);
#11433=(
NAMED_UNIT(*)
PLANE_ANGLE_UNIT()
SI_UNIT($,.RADIAN.)
);
#11434=(
NAMED_UNIT(*)
SI_UNIT($,.STERADIAN.)
SOLID_ANGLE_UNIT()
);
#11442=SHAPE_DEFINITION_REPRESENTATION(#11455,#11485);
#11455=PRODUCT_DEFINITION_SHAPE('',$,#11499);
#11485=SHAPE_REPRESENTATION('',(#4843),#11424);
#11491=PRODUCT_DEFINITION_CONTEXT('part definition',#11532,'design');
#11499=PRODUCT_DEFINITION('2026-10-25-00-55-40-821',
'11_Control_Ball_Stud_M2.5_D5.5',#11512,#11491);
#11512=PRODUCT_DEFINITION_FORMATION('',$,#11541);
#11532=APPLICATION_CONTEXT(
'Core Data for Automotive Mechanical Design Process');
#11533=PRODUCT_CONTEXT('part definition',#11532,'mechanical');
#11541=PRODUCT('2026-10-25-00-55-40-821',
'11_Control_Ball_Stud_M2.5_D5.5',$,(#11533));
#11610=COLOUR_RGB('Black',0.12,0.14,0.17);
#11611=FILL_AREA_STYLE_COLOUR('',#11610);
#11612=FILL_AREA_STYLE('',(#11611));
#11613=SURFACE_STYLE_FILL_AREA(#11612);
#11614=SURFACE_SIDE_STYLE('',(#11613));
#11615=SURFACE_STYLE_USAGE(.BOTH.,#11614);
#11616=PRESENTATION_STYLE_ASSIGNMENT((#11615));
ENDSEC;
END-ISO-10303-21;
